ISO-10303-21;
HEADER;
FILE_DESCRIPTION (('STEP AP214'),
    '1' );
FILE_NAME ( 'ISO 10513 M8 Lock Nut.step', '2026-10-04T02:08:54', ( '' ), ( '' ), 'STEP AP214', 'Unspecified', '' );
FILE_SCHEMA (( 'AUTOMOTIVE_DESIGN' ));
ENDSEC;
DATA;
#2=VERTEX_POINT ( 'NONE', #9971 ) ;
#18=AXIS2_PLACEMENT_3D ( 'NONE', #45673, #23902, #16014 ) ;
#65=VERTEX_POINT ( 'NONE', #33456 ) ;
#69=LINE ( 'NONE', #40323, #2616 ) ;
#80=DIRECTION ( 'NONE',  ( 0.000000000000000000, 0.000000000000000000, 1.000000000000000000 ) ) ;
#83=AXIS2_PLACEMENT_3D ( 'NONE', #20865, #3610, #25184 ) ;
#120=CARTESIAN_POINT ( 'NONE',  ( -0.2559055118110235560, -0.04581480775486102691, -0.03611822492271276469 ) ) ;
#182=CIRCLE ( 'NONE', #27018, 0.1574803149606299191 ) ;
#210=EDGE_LOOP ( 'NONE', ( #1234, #31218, #6999, #28687 ) ) ;
#222=ORIENTED_EDGE ( 'NONE', *, *, #18590, .F. ) ;
#269=LINE ( 'NONE', #3642, #3920 ) ;
#292=CARTESIAN_POINT ( 'NONE',  ( -0.1706040688522822979, -0.1969959271856973060, -0.03730110279448183019 ) ) ;
#340=DIRECTION ( 'NONE',  ( 1.000000000000000000, 0.000000000000000000, 0.000000000000000000 ) ) ;
#357=ORIENTED_EDGE ( 'NONE', *, *, #35134, .F. ) ;
#362=ORIENTED_EDGE ( 'NONE', *, *, #11409, .F. ) ;
#370=VERTEX_POINT ( 'NONE', #31969 ) ;
#415=FACE_OUTER_BOUND ( 'NONE', #12654, .T. ) ;
#440=ORIENTED_EDGE ( 'NONE', *, *, #40777, .T. ) ;
#451=CARTESIAN_POINT ( 'NONE',  ( 0.000000000000000000, 0.000000000000000000, -0.1574803149606298636 ) ) ;
#555=DIRECTION ( 'NONE',  ( 1.000000000000000000, 0.000000000000000000, 0.000000000000000000 ) ) ;
#562=AXIS2_PLACEMENT_3D ( 'NONE', #23103, #45118, #555 ) ;
#584=CARTESIAN_POINT ( 'NONE',  ( 0.000000000000000000, 0.000000000000000000, -0.3149606299212598381 ) ) ;
#632=ADVANCED_FACE ( 'NONE', ( #9505 ), #7574, .F. ) ;
#664=DIRECTION ( 'NONE',  ( 0.000000000000000000, 0.000000000000000000, 1.000000000000000000 ) ) ;
#674=AXIS2_PLACEMENT_3D ( 'NONE', #44945, #41576, #5660 ) ;
#697=CARTESIAN_POINT ( 'NONE',  ( 0.1377952755905511861, 0.000000000000000000, -0.1712639279175142137 ) ) ;
#723=AXIS2_PLACEMENT_3D ( 'NONE', #34044, #1169, #31627 ) ;
#734=AXIS2_PLACEMENT_3D ( 'NONE', #37549, #13067, #42266 ) ;
#742=FACE_OUTER_BOUND ( 'NONE', #45156, .T. ) ;
#752=VERTEX_POINT ( 'NONE', #29469 ) ;
#772=CARTESIAN_POINT ( 'NONE',  ( -0.1574803149606299191, 1.928577636452524610E-17, -0.1966003937007873570 ) ) ;
#839=ADVANCED_FACE ( 'NONE', ( #47393 ), #6059, .T. ) ;
#873=VERTEX_POINT ( 'NONE', #29699 ) ;
#887=CARTESIAN_POINT ( 'NONE',  ( 0.2559052507921502073, -0.04868370062670082654, -0.03721911624063468926 ) ) ;
#920=ORIENTED_EDGE ( 'NONE', *, *, #33954, .T. ) ;
#936=CARTESIAN_POINT ( 'NONE',  ( -0.05425864391566919548, -0.2641663005107283690, -0.3070225280280975411 ) ) ;
#951=CARTESIAN_POINT ( 'NONE',  ( -0.2559127773736598055, 0.03449262457614915567, -0.3136310232799333630 ) ) ;
#953=CIRCLE ( 'NONE', #27790, 0.1377952755905511861 ) ;
#954=VERTEX_POINT ( 'NONE', #1342 ) ;
#957=ORIENTED_EDGE ( 'NONE', *, *, #27196, .F. ) ;
#976=LINE ( 'NONE', #7946, #6077 ) ;
#997=ORIENTED_EDGE ( 'NONE', *, *, #17149, .F. ) ;
#998=EDGE_CURVE ( 'NONE', #41311, #3412, #6808, .T. ) ;
#999=CYLINDRICAL_SURFACE ( 'NONE', #43573, 0.1574803149606299191 ) ;
#1042=SHAPE_REPRESENTATION ( 'ISO 10513 M8 Lock Nut', ( #20860 ), #17833 ) ;
#1085=CARTESIAN_POINT ( 'NONE',  ( 0.1377952755905511861, 0.000000000000000000, -0.2886241641379866385 ) ) ;
#1095=CARTESIAN_POINT ( 'NONE',  ( -0.2341188618557034362, -0.1603256443476437643, -0.2993662881635553719 ) ) ;
#1098=DIRECTION ( 'NONE',  ( 0.000000000000000000, -1.000000000000000000, 0.000000000000000000 ) ) ;
#1103=DIRECTION ( 'NONE',  ( -0.8191520442889914655, 0.000000000000000000, -0.5735764363510464925 ) ) ;
#1161=FACE_OUTER_BOUND ( 'NONE', #10540, .T. ) ;
#1169=DIRECTION ( 'NONE',  ( 0.000000000000000000, 0.000000000000000000, 1.000000000000000000 ) ) ;
#1176=LINE ( 'NONE', #15837, #24099 ) ;
#1179=CARTESIAN_POINT ( 'NONE',  ( 4.268512490100409430E-16, 0.2954942322624074524, -0.2921040715117803055 ) ) ;
#1184=ADVANCED_FACE ( 'NONE', ( #13915 ), #38972, .F. ) ;
#1194=CARTESIAN_POINT ( 'NONE',  ( -0.2559055118110236116, 0.000000000000000000, -0.3149606299212598381 ) ) ;
#1197=ORIENTED_EDGE ( 'NONE', *, *, #33083, .F. ) ;
#1211=CARTESIAN_POINT ( 'NONE',  ( 0.05275478416826926559, 0.2650362434218154761, -0.05809220732314351876 ) ) ;
#1218=CARTESIAN_POINT ( 'NONE',  ( 0.000000000000000000, 0.000000000000000000, -0.1712639279175142137 ) ) ;
#1234=ORIENTED_EDGE ( 'NONE', *, *, #7462, .F. ) ;
#1253=CARTESIAN_POINT ( 'NONE',  ( -0.06594017991609162077, 0.2574235754682526744, -0.3092881115733063790 ) ) ;
#1339=VERTEX_POINT ( 'NONE', #16576 ) ;
#1342=CARTESIAN_POINT ( 'NONE',  ( 0.1377952755905510196, 0.000000000000000000, -0.1828167807439035619 ) ) ;
#1351=ORIENTED_EDGE ( 'NONE', *, *, #3191, .T. ) ;
#1358=FACE_OUTER_BOUND ( 'NONE', #15642, .T. ) ;
#1473=CARTESIAN_POINT ( 'NONE',  ( 0.000000000000000000, 0.000000000000000000, -0.2219368594840610276 ) ) ;
#1478=ORIENTED_EDGE ( 'NONE', *, *, #45701, .T. ) ;
#1500=DIRECTION ( 'NONE',  ( 0.000000000000000000, 0.000000000000000000, 1.000000000000000000 ) ) ;
#1502=CONICAL_SURFACE ( 'NONE', #6088, 0.1377952755905510751, 0.9599310885968951323 ) ;
#1508=CARTESIAN_POINT ( 'NONE',  ( 0.2185580477451977144, -0.1693028889592579356, -0.3031249188859761468 ) ) ;
#1534=DIRECTION ( 'NONE',  ( -1.000000000000000000, 0.000000000000000000, 0.000000000000000000 ) ) ;
#1540=AXIS2_PLACEMENT_3D ( 'NONE', #15602, #11522, #41421 ) ;
#1562=AXIS2_PLACEMENT_3D ( 'NONE', #44292, #23233, #41393 ) ;
#1571=FACE_BOUND ( 'NONE', #4322, .T. ) ;
#1633=CIRCLE ( 'NONE', #30748, 0.1377952755905510751 ) ;
#1635=DIRECTION ( 'NONE',  ( 1.000000000000000000, 0.000000000000000000, 0.000000000000000000 ) ) ;
#1687=CARTESIAN_POINT ( 'NONE',  ( 0.2360031691063811943, 0.1592377390492322742, -0.08759220388355022646 ) ) ;
#1748=VECTOR ( 'NONE', #4428, 39.37007874015748143 ) ;
#1750=DIRECTION ( 'NONE',  ( 0.000000000000000000, 0.000000000000000000, 1.000000000000000000 ) ) ;
#1800=CARTESIAN_POINT ( 'NONE',  ( 0.1574803149606299191, 0.000000000000000000, -0.1574803149606298636 ) ) ;
#1841=CARTESIAN_POINT ( 'NONE',  ( -0.2133366555409255683, 0.1723185650271337466, -0.3044102143376714031 ) ) ;
#1846=VERTEX_POINT ( 'NONE', #36083 ) ;
#1855=CARTESIAN_POINT ( 'NONE',  ( -0.2559055118110236671, 0.1226799225465883270, -0.2993403469937337413 ) ) ;
#1862=CARTESIAN_POINT ( 'NONE',  ( 0.000000000000000000, 0.000000000000000000, -0.3149606299212598381 ) ) ;
#1866=CARTESIAN_POINT ( 'NONE',  ( 0.2559055118110236116, -0.1477471161312047254, -0.3149606299212598381 ) ) ;
#1941=EDGE_CURVE ( 'NONE', #14850, #38506, #16810, .T. ) ;
#1943=B_SPLINE_CURVE_WITH_KNOTS ( 'NONE', 3,
 ( #19400, #45017, #30232, #8373, #34051, #12230, #936, #26137, #26853, #5019, #40705, #30459, #44544, #4520, #22759, #37613, #44087, #33341, #23001 ),
 .UNSPECIFIED., .F., .F.,
 ( 4, 2, 2, 1, 2, 2, 2, 2, 2, 4 ),
 ( 0.000000000000000000, 0.2500000000000015543, 0.3750000000000021649, 0.4375000000000022760, 0.4687500000000021649, 0.5000000000000021094, 0.6250000000000014433, 0.6875000000000008882, 0.7500000000000004441, 1.000000000000000000 ),
 .UNSPECIFIED. ) ;
#1944=VECTOR ( 'NONE', #31591, 39.37007874015748143 ) ;
#2016=CARTESIAN_POINT ( 'NONE',  ( 0.1578366172104690157, 0.2043672459940823471, -0.3136338785705632959 ) ) ;
#2027=ORIENTED_EDGE ( 'NONE', *, *, #23171, .T. ) ;
#2041=CARTESIAN_POINT ( 'NONE',  ( -0.2559055118110236116, 0.1477471161312031434, -0.1122047244094468571 ) ) ;
#2065=ADVANCED_FACE ( 'NONE', ( #27224 ), #1502, .F. ) ;
#2101=DIRECTION ( 'NONE',  ( 0.000000000000000000, 0.000000000000000000, 1.000000000000000000 ) ) ;
#2102=ORIENTED_EDGE ( 'NONE', *, *, #35592, .F. ) ;
#2135=AXIS2_PLACEMENT_3D ( 'NONE', #14937, #21886, #25004 ) ;
#2153=CIRCLE ( 'NONE', #15974, 0.1574803149606299191 ) ;
#2191=EDGE_LOOP ( 'NONE', ( #41545, #6382, #11816, #21573 ) ) ;
#2192=CARTESIAN_POINT ( 'NONE',  ( 0.000000000000000000, 0.000000000000000000, -0.1436967020037460685 ) ) ;
#2221=CARTESIAN_POINT ( 'NONE',  ( 0.2559055118110235560, 0.07338436260360474417, -0.3090062946576829783 ) ) ;
#2243=CARTESIAN_POINT ( 'NONE',  ( 0.1550611416720020230, 0.2059691479692354332, -0.3138705397960873111 ) ) ;
#2249=ORIENTED_EDGE ( 'NONE', *, *, #23334, .F. ) ;
#2251=CARTESIAN_POINT ( 'NONE',  ( 0.1934636958948905971, -0.1837979153590739156, -0.05069326177276377299 ) ) ;
#2265=AXIS2_PLACEMENT_3D ( 'NONE', #23060, #44845, #19691 ) ;
#2269=EDGE_CURVE ( 'NONE', #31572, #34936, #15953, .T. ) ;
#2275=CARTESIAN_POINT ( 'NONE',  ( -0.1702179831425296441, 0.1972188338741525382, -0.03726912461314065700 ) ) ;
#2355=DIRECTION ( 'NONE',  ( -0.000000000000000000, -0.000000000000000000, -1.000000000000000000 ) ) ;
#2379=CIRCLE ( 'NONE', #29242, 0.1574803149606299191 ) ;
#2381=( NAMED_UNIT ( * ) SI_UNIT ( $, .STERADIAN. ) SOLID_ANGLE_UNIT ( ) ) ;
#2391=CARTESIAN_POINT ( 'NONE',  ( 0.1339681929923581538, 0.2181476599754205714, -0.02739586109244947915 ) ) ;
#2395=ORIENTED_EDGE ( 'NONE', *, *, #29884, .F. ) ;
#2414=AXIS2_PLACEMENT_3D ( 'NONE', #20561, #20331, #35436 ) ;
#2415=CARTESIAN_POINT ( 'NONE',  ( -0.1574803149606299191, 0.000000000000000000, -0.07924015748031493223 ) ) ;
#2424=ORIENTED_EDGE ( 'NONE', *, *, #32883, .T. ) ;
#2451=LINE ( 'NONE', #35773, #17015 ) ;
#2483=CARTESIAN_POINT ( 'NONE',  ( 0.2031507276427542419, -0.1782051049717964242, -0.05809220732314481633 ) ) ;
#2495=AXIS2_PLACEMENT_3D ( 'NONE', #41273, #45592, #27204 ) ;
#2555=CARTESIAN_POINT ( 'NONE',  ( -0.2559055569979697409, 0.07184629814250909075, -0.3092506151682454241 ) ) ;
#2568=DIRECTION ( 'NONE',  ( 1.000000000000000000, 0.000000000000000000, 0.000000000000000000 ) ) ;
#2585=ADVANCED_FACE ( 'NONE', ( #32325 ), #47154, .F. ) ;
#2616=VECTOR ( 'NONE', #7747, 39.37007874015748143 ) ;
#2617=CARTESIAN_POINT ( 'NONE',  ( 0.1377952755905511861, 0.000000000000000000, -0.09302377043719921301 ) ) ;
#2623=CARTESIAN_POINT ( 'NONE',  ( 0.05770278849818187561, -0.2621795117899916594, -0.05428606100832126385 ) ) ;
#2629=VERTEX_POINT ( 'NONE', #35207 ) ;
#2650=EDGE_LOOP ( 'NONE', ( #10832, #39250, #33625, #36885 ) ) ;
#2659=CARTESIAN_POINT ( 'NONE',  ( -0.1377952755905509641, 0.000000000000000000, -0.06545654452343109553 ) ) ;
#2670=CARTESIAN_POINT ( 'NONE',  ( 0.000000000000000000, 0.000000000000000000, -0.3001770169643759867 ) ) ;
#2689=CARTESIAN_POINT ( 'NONE',  ( 0.2559055118110236671, 0.01223568982215688349, -0.3149606299212600047 ) ) ;
#2692=ORIENTED_EDGE ( 'NONE', *, *, #35134, .T. ) ;
#2694=CARTESIAN_POINT ( 'NONE',  ( 0.2133366555414178134, -0.1723185650269667135, -0.3044102143375118641 ) ) ;
#2712=DIRECTION ( 'NONE',  ( 1.000000000000000000, 0.000000000000000000, 0.000000000000000000 ) ) ;
#2725=ORIENTED_EDGE ( 'NONE', *, *, #23101, .F. ) ;
#2733=DIRECTION ( 'NONE',  ( 1.000000000000000000, 0.000000000000000000, 0.000000000000000000 ) ) ;
#2737=ADVANCED_FACE ( 'NONE', ( #13849 ), #7740, .F. ) ;
#2799=CARTESIAN_POINT ( 'NONE',  ( -0.1574803149606299191, 0.000000000000000000, -0.1966003937007873570 ) ) ;
#2805=FACE_OUTER_BOUND ( 'NONE', #13667, .T. ) ;
#2829=CARTESIAN_POINT ( 'NONE',  ( 0.2559055051320487939, 0.04218512718539534079, -0.03480397727850505912 ) ) ;
#2849=CARTESIAN_POINT ( 'NONE',  ( 0.09240388072374286499, -0.2421448268523899161, -0.03441347972012361728 ) ) ;
#2933=LINE ( 'NONE', #17570, #8261 ) ;
#2942=CARTESIAN_POINT ( 'NONE',  ( 0.2001839496640331895, -0.1799179750364369168, -0.05578523004296986193 ) ) ;
#2951=VERTEX_POINT ( 'NONE', #7536 ) ;
#2957=EDGE_CURVE ( 'NONE', #4869, #17741, #22386, .T. ) ;
#2966=CARTESIAN_POINT ( 'NONE',  ( -0.09162190804155563584, 0.2425962989909478396, -0.03472289316813708532 ) ) ;
#3018=EDGE_CURVE ( 'NONE', #40880, #7920, #44183, .T. ) ;
#3024=CIRCLE ( 'NONE', #723, 0.2559055118110236116 ) ;
#3039=CIRCLE ( 'NONE', #11473, 0.1574803149606299191 ) ;
#3046=CARTESIAN_POINT ( 'NONE',  ( 0.000000000000000000, 0.000000000000000000, -0.2748405511811023438 ) ) ;
#3066=VECTOR ( 'NONE', #30402, 39.37007874015748143 ) ;
#3129=CARTESIAN_POINT ( 'NONE',  ( 0.1377952755905509641, 0.000000000000000000, -0.06545654452343109553 ) ) ;
#3163=CARTESIAN_POINT ( 'NONE',  ( 0.2559055118110235005, 0.05276756496564156268, -0.3119197741533752954 ) ) ;
#3191=EDGE_CURVE ( 'NONE', #41717, #2, #33783, .T. ) ;
#3197=EDGE_CURVE ( 'NONE', #38861, #65, #15496, .T. ) ;
#3208=AXIS2_PLACEMENT_3D ( 'NONE', #14187, #36698, #3857 ) ;
#3263=EDGE_LOOP ( 'NONE', ( #21572, #9337, #26416, #43733, #38615 ) ) ;
#3266=ORIENTED_EDGE ( 'NONE', *, *, #24133, .T. ) ;
#3286=CARTESIAN_POINT ( 'NONE',  ( 0.000000000000000000, 0.000000000000000000, -0.1712639279175142137 ) ) ;
#3293=EDGE_LOOP ( 'NONE', ( #20466, #20335, #40495, #27925 ) ) ;
#3347=DIRECTION ( 'NONE',  ( 0.000000000000000000, 0.000000000000000000, 1.000000000000000000 ) ) ;
#3365=STYLED_ITEM ( 'NONE', ( #18942 ), #4462 ) ;
#3412=VERTEX_POINT ( 'NONE', #15752 ) ;
#3461=EDGE_CURVE ( 'NONE', #4309, #26963, #33599, .T. ) ;
#3506=CARTESIAN_POINT ( 'NONE',  ( -0.1939344384856130921, 0.1835261454399950420, -0.3085539532670508178 ) ) ;
#3530=AXIS2_PLACEMENT_3D ( 'NONE', #41738, #30779, #8222 ) ;
#3540=B_SPLINE_CURVE_WITH_KNOTS ( 'NONE', 3,
 ( #8889, #33849, #4804, #15626, #45048, #1211, #12261, #15150, #30265, #12027, #26652, #16336, #41919, #30957, #27377, #28070, #45523, #20845, #23994, #9371, #13659, #2391, #46008, #10072, #17258, #31897, #9611, #39051, #24230, #24450, #12974, #16559, #39285, #19904, #5768, #35013, #42408, #12747, #6221, #1687, #35486 ),
 .UNSPECIFIED., .F., .F.,
 ( 4, 1, 1, 1, 1, 1, 1, 2, 2, 1, 1, 1, 1, 2, 2, 2, 1, 1, 1, 1, 2, 2, 1, 1, 1, 1, 1, 2, 2, 4 ),
 ( 0.000000000000000000, 0.1249999999999960865, 0.1874999999999940326, 0.2187499999999930334, 0.2343749999999925338, 0.2421874999999922562, 0.2460937499999920341, 0.2480468749999919786, 0.2499999999999919231, 0.3124999999999915068, 0.3437499999999912292, 0.3593749999999910627, 0.3671874999999910627, 0.3710937499999910627, 0.3749999999999910072, 0.4999999999999903411, 0.5624999999999898970, 0.5937499999999898970, 0.6093749999999897859, 0.6171874999999897859, 0.6210937499999897859, 0.6249999999999897859, 0.6874999999999873435, 0.7187499999999860112, 0.7343749999999855671, 0.7421874999999853451, 0.7460937499999852340, 0.7480468749999852340, 0.7499999999999852340, 1.000000000000000000 ),
 .UNSPECIFIED. ) ;
#3589=CARTESIAN_POINT ( 'NONE',  ( 3.414809992080330995E-16, 0.2954942322624074524, -0.3149606299212598381 ) ) ;
#3606=VERTEX_POINT ( 'NONE', #32002 ) ;
#3610=DIRECTION ( 'NONE',  ( 0.000000000000000000, 0.000000000000000000, 1.000000000000000000 ) ) ;
#3642=CARTESIAN_POINT ( 'NONE',  ( -0.1377952755905510474, 0.000000000000000000, -0.2610569382242185488 ) ) ;
#3663=CARTESIAN_POINT ( 'NONE',  ( -0.08812199945791716893, -0.2446169721538513642, -0.03618545512905850525 ) ) ;
#3724=CARTESIAN_POINT ( 'NONE',  ( -0.2559055118110236116, -0.1477471161312049197, -0.1122047244094488277 ) ) ;
#3755=CARTESIAN_POINT ( 'NONE',  ( -0.2559055118110236116, 0.007127922025054847163, -0.02740704184215039807 ) ) ;
#3757=EDGE_CURVE ( 'NONE', #30017, #22098, #35438, .T. ) ;
#3761=ORIENTED_EDGE ( 'NONE', *, *, #5244, .F. ) ;
#3764=AXIS2_PLACEMENT_3D ( 'NONE', #43714, #10917, #3931 ) ;
#3774=FACE_OUTER_BOUND ( 'NONE', #21502, .T. ) ;
#3788=DIRECTION ( 'NONE',  ( -1.000000000000000000, 0.000000000000000000, 0.000000000000000000 ) ) ;
#3799=VERTEX_POINT ( 'NONE', #2799 ) ;
#3819=DIRECTION ( 'NONE',  ( 0.000000000000000000, 0.000000000000000000, 1.000000000000000000 ) ) ;
#3853=DIRECTION ( 'NONE',  ( 0.000000000000000000, 0.000000000000000000, 1.000000000000000000 ) ) ;
#3857=DIRECTION ( 'NONE',  ( 1.000000000000000000, 0.000000000000000000, 0.000000000000000000 ) ) ;
#3872=DIRECTION ( 'NONE',  ( 0.8191520442889980158, 1.003171929053532266E-16, -0.5735764363510372776 ) ) ;
#3887=DIRECTION ( 'NONE',  ( 0.000000000000000000, 0.000000000000000000, 1.000000000000000000 ) ) ;
#3891=CARTESIAN_POINT ( 'NONE',  ( -0.1595947434768149320, -0.2033521641548195757, -0.03294411891278189314 ) ) ;
#3905=CIRCLE ( 'NONE', #30723, 0.1377952755905510196 ) ;
#3920=VECTOR ( 'NONE', #28608, 39.37007874015748143 ) ;
#3931=DIRECTION ( 'NONE',  ( 1.000000000000000000, 0.000000000000000000, 0.000000000000000000 ) ) ;
#3936=CARTESIAN_POINT ( 'NONE',  ( 0.000000000000000000, 0.000000000000000000, -0.2610569382242185488 ) ) ;
#3946=DIRECTION ( 'NONE',  ( -0.000000000000000000, -0.000000000000000000, -1.000000000000000000 ) ) ;
#3959=CARTESIAN_POINT ( 'NONE',  ( -0.2559055118110235560, -0.08321452205036067307, -0.05565866801132852287 ) ) ;
#3964=CARTESIAN_POINT ( 'NONE',  ( -0.1871882013107595277, 0.1874210200769348689, -0.3098131533095127010 ) ) ;
#3994=CIRCLE ( 'NONE', #30835, 0.1377952755905511861 ) ;
#4019=CARTESIAN_POINT ( 'NONE',  ( 0.2559043039006217990, -0.06897312490620088887, -0.04680397461132097814 ) ) ;
#4026=VECTOR ( 'NONE', #38304, 39.37007874015748854 ) ;
#4063=ORIENTED_EDGE ( 'NONE', *, *, #31353, .F. ) ;
#4068=AXIS2_PLACEMENT_3D ( 'NONE', #37085, #22707, #4234 ) ;
#4092=EDGE_CURVE ( 'NONE', #31834, #16796, #4674, .T. ) ;
#4098=DIRECTION ( 'NONE',  ( 0.000000000000000000, 0.000000000000000000, 1.000000000000000000 ) ) ;
#4119=CARTESIAN_POINT ( 'NONE',  ( -0.08985779549332877092, -0.2436148098455482858, -0.03544556188504763977 ) ) ;
#4157=CIRCLE ( 'NONE', #26400, 0.1377952755905509641 ) ;
#4187=EDGE_CURVE ( 'NONE', #26918, #1846, #23978, .T. ) ;
#4188=CARTESIAN_POINT ( 'NONE',  ( -0.1387951811623720499, 0.2153607970560884322, -0.3149606299212598381 ) ) ;
#4201=ADVANCED_FACE ( 'NONE', ( #21360 ), #17048, .F. ) ;
#4219=ORIENTED_EDGE ( 'NONE', *, *, #21706, .F. ) ;
#4234=DIRECTION ( 'NONE',  ( 1.000000000000000000, 0.000000000000000000, 0.000000000000000000 ) ) ;
#4240=CARTESIAN_POINT ( 'NONE',  ( 0.2559055118110236116, -4.594920972184172978E-16, -0.02740704184215071032 ) ) ;
#4246=CIRCLE ( 'NONE', #26398, 0.1377952755905511861 ) ;
#4260=ORIENTED_EDGE ( 'NONE', *, *, #34875, .T. ) ;
#4303=ORIENTED_EDGE ( 'NONE', *, *, #18459, .T. ) ;
#4309=VERTEX_POINT ( 'NONE', #17534 ) ;
#4321=CARTESIAN_POINT ( 'NONE',  ( -0.1574803149606299191, 0.000000000000000000, -0.0009999999999999347518 ) ) ;
#4322=EDGE_LOOP ( 'NONE', ( #23508, #9476 ) ) ;
#4344=DIRECTION ( 'NONE',  ( 0.000000000000000000, 0.000000000000000000, 1.000000000000000000 ) ) ;
#4348=ORIENTED_EDGE ( 'NONE', *, *, #28268, .T. ) ;
#4349=ADVANCED_FACE ( 'NONE', ( #32168 ), #41573, .T. ) ;
#4350=CARTESIAN_POINT ( 'NONE',  ( 0.000000000000000000, 0.000000000000000000, -0.3149606299212598381 ) ) ;
#4358=CARTESIAN_POINT ( 'NONE',  ( -0.2559097037360847371, 0.05003845355613480150, -0.3122011391401430802 ) ) ;
#4365=VECTOR ( 'NONE', #28429, 39.37007874015748143 ) ;
#4389=DIRECTION ( 'NONE',  ( 0.000000000000000000, 0.000000000000000000, 1.000000000000000000 ) ) ;
#4418=CARTESIAN_POINT ( 'NONE',  ( -0.1657973489137827550, 0.1997733981813884230, -0.3128311589625774047 ) ) ;
#4428=DIRECTION ( 'NONE',  ( 0.000000000000000000, 0.000000000000000000, 1.000000000000000000 ) ) ;
#4462=MANIFOLD_SOLID_BREP ( 'ISO 10513 M8 Lock Nut', #14905 ) ;
#4520=CARTESIAN_POINT ( 'NONE',  ( -0.08476992594631420352, -0.2465534299915450589, -0.3121915932859496423 ) ) ;
#4537=EDGE_LOOP ( 'NONE', ( #25418, #27235, #19220, #19481 ) ) ;
#4541=CIRCLE ( 'NONE', #17594, 0.1377952755905510196 ) ;
#4557=LINE ( 'NONE', #36708, #16259 ) ;
#4565=FACE_OUTER_BOUND ( 'NONE', #13758, .T. ) ;
#4580=CARTESIAN_POINT ( 'NONE',  ( 0.000000000000000000, 0.000000000000000000, -0.2357204724409448504 ) ) ;
#4659=VECTOR ( 'NONE', #30111, 39.37007874015748143 ) ;
#4674=LINE ( 'NONE', #20423, #1748 ) ;
#4675=CIRCLE ( 'NONE', #8518, 0.2559055118110236116 ) ;
#4676=CIRCLE ( 'NONE', #26052, 0.1377952755905511861 ) ;
#4692=CARTESIAN_POINT ( 'NONE',  ( 0.1574803149606299191, 0.000000000000000000, -0.2357204724409448504 ) ) ;
#4721=CARTESIAN_POINT ( 'NONE',  ( 0.1377952755905509363, 0.000000000000000000, -0.1045766232635885612 ) ) ;
#4737=DIRECTION ( 'NONE',  ( 0.000000000000000000, 0.000000000000000000, 1.000000000000000000 ) ) ;
#4798=CARTESIAN_POINT ( 'NONE',  ( 0.2133350748051826562, 0.1723249637083595076, -0.3049284531894324579 ) ) ;
#4804=CARTESIAN_POINT ( 'NONE',  ( 0.02440571223928530292, 0.2814035877312904832, -0.08364281214760876937 ) ) ;
#4813=CARTESIAN_POINT ( 'NONE',  ( 0.2431102362204724532, 2.977241726273585582E-17, 0.000000000000000000 ) ) ;
#4829=ORIENTED_EDGE ( 'NONE', *, *, #22956, .T. ) ;
#4848=CARTESIAN_POINT ( 'NONE',  ( -0.1008439437003635641, 0.2372714618127385600, -0.3138705397960871446 ) ) ;
#4868=CARTESIAN_POINT ( 'NONE',  ( 0.1574803149606299191, 0.000000000000000000, -0.04012007874015743186 ) ) ;
#4869=VERTEX_POINT ( 'NONE', #36182 ) ;
#4870=B_SPLINE_CURVE_WITH_KNOTS ( 'NONE', 3,
 ( #24078, #6303, #31507, #46089, #32460, #40532, #17813, #7721, #36733, #26199, #29119, #10881, #25501, #43431, #7269, #3663, #40303, #4119, #40765, #14459, #22105, #29600, #21887, #18286, #3891, #36508, #33170, #39831, #18518, #292, #32691, #14938, #25732, #44142, #33401, #32928, #43910, #21648, #11340, #11112, #25953 ),
 .UNSPECIFIED., .F., .F.,
 ( 4, 1, 1, 1, 1, 1, 1, 2, 2, 1, 1, 1, 1, 2, 2, 2, 1, 1, 1, 1, 2, 2, 1, 1, 1, 1, 1, 2, 2, 4 ),
 ( 0.000000000000000000, 0.1250000000000038858, 0.1875000000000058287, 0.2187500000000068001, 0.2343750000000072164, 0.2421875000000074107, 0.2460937500000075495, 0.2480468750000075773, 0.2500000000000076050, 0.3125000000000083822, 0.3437500000000087153, 0.3593750000000088263, 0.3671875000000089373, 0.3710937500000089373, 0.3750000000000089373, 0.5000000000000056621, 0.5625000000000042188, 0.5937500000000035527, 0.6093750000000032196, 0.6171875000000029976, 0.6210937500000028866, 0.6250000000000027756, 0.6875000000000032196, 0.7187500000000033307, 0.7343750000000035527, 0.7421875000000035527, 0.7460937500000036637, 0.7480468750000035527, 0.7500000000000035527, 1.000000000000000000 ),
 .UNSPECIFIED. ) ;
#4871=CARTESIAN_POINT ( 'NONE',  ( 0.000000000000000000, 0.000000000000000000, 0.000000000000000000 ) ) ;
#4913=EDGE_LOOP ( 'NONE', ( #6162, #39201, #38762, #43388 ) ) ;
#4991=CONICAL_SURFACE ( 'NONE', #34891, 0.1377952755905510474, 0.9599310885968920237 ) ;
#5002=ORIENTED_EDGE ( 'NONE', *, *, #3197, .T. ) ;
#5004=ORIENTED_EDGE ( 'NONE', *, *, #28278, .F. ) ;
#5019=CARTESIAN_POINT ( 'NONE',  ( -0.06197108496686676293, -0.2597152231171959147, -0.3085539532670581453 ) ) ;
#5058=DIRECTION ( 'NONE',  ( 0.000000000000000000, 0.000000000000000000, 1.000000000000000000 ) ) ;
#5090=LINE ( 'NONE', #45093, #36106 ) ;
#5108=DIRECTION ( 'NONE',  ( -0.8191520442889873577, 1.003171929053519323E-16, 0.5735764363510523767 ) ) ;
#5225=FACE_OUTER_BOUND ( 'NONE', #36959, .T. ) ;
#5238=CARTESIAN_POINT ( 'NONE',  ( 0.000000000000000000, 0.000000000000000000, -0.1966003937007873570 ) ) ;
#5244=EDGE_CURVE ( 'NONE', #40024, #4309, #17214, .T. ) ;
#5245=LINE ( 'NONE', #41882, #19114 ) ;
#5249=EDGE_LOOP ( 'NONE', ( #9452, #42557, #37488, #38675 ) ) ;
#5257=CARTESIAN_POINT ( 'NONE',  ( 0.05814395269904383545, 0.2619241685425472421, -0.3078067560681213566 ) ) ;
#5302=ADVANCED_FACE ( 'NONE', ( #16955 ), #34099, .T. ) ;
#5304=FACE_OUTER_BOUND ( 'NONE', #39541, .T. ) ;
#5380=FACE_OUTER_BOUND ( 'NONE', #46586, .T. ) ;
#5437=CARTESIAN_POINT ( 'NONE',  ( 0.000000000000000000, 0.000000000000000000, -0.2357204724409448504 ) ) ;
#5451=DIRECTION ( 'NONE',  ( 1.000000000000000000, 0.000000000000000000, 0.000000000000000000 ) ) ;
#5456=CARTESIAN_POINT ( 'NONE',  ( 0.000000000000000000, 0.000000000000000000, -0.3149606299212598381 ) ) ;
#5511=AXIS2_PLACEMENT_3D ( 'NONE', #8642, #5527, #42166 ) ;
#5514=AXIS2_PLACEMENT_3D ( 'NONE', #32162, #43872, #39786 ) ;
#5515=CONICAL_SURFACE ( 'NONE', #6252, 0.2559055118110236116, 1.047197551196597409 ) ;
#5522=EDGE_CURVE ( 'NONE', #5631, #20308, #34561, .T. ) ;
#5527=DIRECTION ( 'NONE',  ( 0.000000000000000000, 0.000000000000000000, 1.000000000000000000 ) ) ;
#5529=CONICAL_SURFACE ( 'NONE', #32314, 0.2559055118110236116, 1.047197551196597409 ) ;
#5532=DIRECTION ( 'NONE',  ( 1.000000000000000000, 0.000000000000000000, 0.000000000000000000 ) ) ;
#5535=AXIS2_PLACEMENT_3D ( 'NONE', #42005, #33936, #12354 ) ;
#5547=CARTESIAN_POINT ( 'NONE',  ( 0.000000000000000000, 0.000000000000000000, -0.0009999999999999347518 ) ) ;
#5552=PRODUCT ( 'ISO 10513 M8 Lock Nut', 'ISO 10513 M8 Lock Nut', '', ( #18543 ) ) ;
#5567=ADVANCED_FACE ( 'NONE', ( #27404 ), #43992, .F. ) ;
#5591=CARTESIAN_POINT ( 'NONE',  ( 0.000000000000000000, 0.000000000000000000, -0.3149606299212598381 ) ) ;
#5631=VERTEX_POINT ( 'NONE', #3129 ) ;
#5643=CARTESIAN_POINT ( 'NONE',  ( -0.2314997995717629486, 0.1618377606623054299, -0.08364281214763795436 ) ) ;
#5660=DIRECTION ( 'NONE',  ( 1.000000000000000000, 0.000000000000000000, 0.000000000000000000 ) ) ;
#5699=LINE ( 'NONE', #26588, #30955 ) ;
#5709=DIRECTION ( 'NONE',  ( -0.8191520442889991260, 0.000000000000000000, -0.5735764363510356123 ) ) ;
#5715=FACE_OUTER_BOUND ( 'NONE', #34114, .T. ) ;
#5735=CARTESIAN_POINT ( 'NONE',  ( 0.09272654090495630053, 0.2419614285902424167, -0.3131151337379057265 ) ) ;
#5754=AXIS2_PLACEMENT_3D ( 'NONE', #2192, #3853, #35977 ) ;
#5768=CARTESIAN_POINT ( 'NONE',  ( 0.1976644210311565564, 0.1813726255708565105, -0.05388431474955820977 ) ) ;
#5771=AXIS2_PLACEMENT_3D ( 'NONE', #451, #3819, #11268 ) ;
#5809=CARTESIAN_POINT ( 'NONE',  ( -0.06863485658886912810, 0.2558675481231191817, -0.3097625555228274985 ) ) ;
#5819=CARTESIAN_POINT ( 'NONE',  ( 0.2559055118110235560, -0.02431590950899893341, -0.3149606299212598381 ) ) ;
#5834=CARTESIAN_POINT ( 'NONE',  ( 0.1818270763438056270, -0.1905157801853442356, -0.3106979152243058984 ) ) ;
#5854=CARTESIAN_POINT ( 'NONE',  ( 0.1469224761503790389, 0.2106668292956904442, -0.3144321013757216399 ) ) ;
#5876=CARTESIAN_POINT ( 'NONE',  ( -0.2559053909010672312, -0.07743436953536136924, -0.3083471293668692548 ) ) ;
#5884=CARTESIAN_POINT ( 'NONE',  ( -0.1934636958948592889, 0.1837979153590902914, -0.05069326177273324185 ) ) ;
#5927=EDGE_LOOP ( 'NONE', ( #362, #35144, #21456, #1197 ) ) ;
#5957=ORIENTED_EDGE ( 'NONE', *, *, #25512, .T. ) ;
#5992=ADVANCED_FACE ( 'NONE', ( #7610 ), #4991, .F. ) ;
#6059=CONICAL_SURFACE ( 'NONE', #23667, 0.2559055118110236116, 1.047197551196597409 ) ;
#6072=ORIENTED_EDGE ( 'NONE', *, *, #17257, .F. ) ;
#6077=VECTOR ( 'NONE', #30271, 39.37007874015748143 ) ;
#6088=AXIS2_PLACEMENT_3D ( 'NONE', #45143, #19284, #1534 ) ;
#6094=CARTESIAN_POINT ( 'NONE',  ( -0.09240388072374362827, 0.2421448268523877234, -0.03441347972012046702 ) ) ;
#6098=ADVANCED_FACE ( 'NONE', ( #43507 ), #24836, .T. ) ;
#6122=DIRECTION ( 'NONE',  ( 0.8191520442889914655, 1.003171929053524500E-16, -0.5735764363510464925 ) ) ;
#6151=DIRECTION ( 'NONE',  ( 1.000000000000000000, 0.000000000000000000, 0.000000000000000000 ) ) ;
#6162=ORIENTED_EDGE ( 'NONE', *, *, #37493, .F. ) ;
#6164=CARTESIAN_POINT ( 'NONE',  ( 0.000000000000000000, 0.000000000000000000, -0.2103840066576717072 ) ) ;
#6190=CARTESIAN_POINT ( 'NONE',  ( 0.1279527559055118058, 0.2216206741968047289, -0.3149606299212598381 ) ) ;
#6215=EDGE_CURVE ( 'NONE', #23237, #38700, #29554, .T. ) ;
#6218=CARTESIAN_POINT ( 'NONE',  ( 0.1528603379501230763, -0.2072402749984882109, -0.03001342526389988788 ) ) ;
#6221=CARTESIAN_POINT ( 'NONE',  ( 0.2170082705493531494, 0.1702044488443620607, -0.06846571731933490113 ) ) ;
#6252=AXIS2_PLACEMENT_3D ( 'NONE', #21983, #32560, #29233 ) ;
#6282=DIRECTION ( 'NONE',  ( 0.000000000000000000, 0.000000000000000000, 1.000000000000000000 ) ) ;
#6283=CARTESIAN_POINT ( 'NONE',  ( 0.2559055118110235560, 0.07179175674853267852, -0.3092570035108861415 ) ) ;
#6290=CARTESIAN_POINT ( 'NONE',  ( 0.1939344384855389569, -0.1835261454400549941, -0.3085539532670578677 ) ) ;
#6303=CARTESIAN_POINT ( 'NONE',  ( -0.009895589093224880714, -0.2897810112356447587, -0.09996720075265054517 ) ) ;
#6382=ORIENTED_EDGE ( 'NONE', *, *, #21253, .T. ) ;
#6387=ORIENTED_EDGE ( 'NONE', *, *, #28433, .T. ) ;
#6423=VERTEX_POINT ( 'NONE', #30588 ) ;
#6437=CARTESIAN_POINT ( 'NONE',  ( 0.2559055118110235560, 0.1252082647764977408, -0.08806600079302280559 ) ) ;
#6440=CARTESIAN_POINT ( 'NONE',  ( 0.1567662409572586624, 1.919832752026695389E-17, -0.0004999999999998990712 ) ) ;
#6458=CARTESIAN_POINT ( 'NONE',  ( 0.08530144295876790350, -0.2462454212079008276, -0.03730110279447364230 ) ) ;
#6510=CARTESIAN_POINT ( 'NONE',  ( 0.2559055118110236671, -0.07952748568939312090, -0.3079936629965072115 ) ) ;
#6523=CIRCLE ( 'NONE', #8066, 0.1377952755905509641 ) ;
#6527=CARTESIAN_POINT ( 'NONE',  ( 0.2016454051087482324, -0.1790725142610753162, -0.3070225280279249569 ) ) ;
#6562=CARTESIAN_POINT ( 'NONE',  ( 0.000000000000000000, 0.000000000000000000, -0.3149606299212598381 ) ) ;
#6600=EDGE_LOOP ( 'NONE', ( #13462, #35039, #19151 ) ) ;
#6602=EDGE_CURVE ( 'NONE', #31572, #25178, #8920, .T. ) ;
#6645=CARTESIAN_POINT ( 'NONE',  ( -0.1574803149606299191, 1.928577636452524610E-17, -0.1574803149606298636 ) ) ;
#6703=ADVANCED_FACE ( 'NONE', ( #16715 ), #31346, .F. ) ;
#6718=FACE_OUTER_BOUND ( 'NONE', #13424, .T. ) ;
#6740=CARTESIAN_POINT ( 'NONE',  ( 0.000000000000000000, 0.000000000000000000, -0.06545654452343109553 ) ) ;
#6741=DIRECTION ( 'NONE',  ( 1.000000000000000000, 0.000000000000000000, 0.000000000000000000 ) ) ;
#6752=DIRECTION ( 'NONE',  ( 0.000000000000000000, 0.000000000000000000, 1.000000000000000000 ) ) ;
#6757=DIRECTION ( 'NONE',  ( 1.000000000000000000, 0.000000000000000000, 0.000000000000000000 ) ) ;
#6808=CIRCLE ( 'NONE', #674, 0.1377952755905511861 ) ;
#6895=DIRECTION ( 'NONE',  ( -1.000000000000000000, 0.000000000000000000, 0.000000000000000000 ) ) ;
#6901=VECTOR ( 'NONE', #36881, 39.37007874015748143 ) ;
#6914=ORIENTED_EDGE ( 'NONE', *, *, #37069, .T. ) ;
#6931=EDGE_CURVE ( 'NONE', #2, #41717, #4246, .T. ) ;
#6933=CARTESIAN_POINT ( 'NONE',  ( 0.1702179831425535972, -0.1972188338741404368, -0.03726912461316504721 ) ) ;
#6951=EDGE_LOOP ( 'NONE', ( #38270, #33709, #28283, #32704 ) ) ;
#6980=CIRCLE ( 'NONE', #45240, 0.1377952755905509641 ) ;
#6999=ORIENTED_EDGE ( 'NONE', *, *, #3018, .T. ) ;
#7054=CARTESIAN_POINT ( 'NONE',  ( -0.2559055118110236116, -0.1477471161312043368, -0.3149606299212598381 ) ) ;
#7077=DIRECTION ( 'NONE',  ( 0.000000000000000000, 0.000000000000000000, 1.000000000000000000 ) ) ;
#7125=DIRECTION ( 'NONE',  ( 1.000000000000000000, 0.000000000000000000, 0.000000000000000000 ) ) ;
#7132=ORIENTED_EDGE ( 'NONE', *, *, #5522, .T. ) ;
#7143=ORIENTED_EDGE ( 'NONE', *, *, #10415, .F. ) ;
#7144=CARTESIAN_POINT ( 'NONE',  ( 0.000000000000000000, 0.000000000000000000, -0.1436967020037460685 ) ) ;
#7177=AXIS2_PLACEMENT_3D ( 'NONE', #19378, #41513, #38191 ) ;
#7200=EDGE_CURVE ( 'NONE', #26963, #40024, #24874, .T. ) ;
#7227=( CONVERSION_BASED_UNIT ( 'INCH', #36473 ) LENGTH_UNIT ( ) NAMED_UNIT ( #30168 ) ) ;
#7269=CARTESIAN_POINT ( 'NONE',  ( -0.08568752866851420125, -0.2460225145194475105, -0.03726912461313686836 ) ) ;
#7313=VERTEX_POINT ( 'NONE', #10424 ) ;
#7337=ORIENTED_EDGE ( 'NONE', *, *, #32450, .T. ) ;
#7340=CARTESIAN_POINT ( 'NONE',  ( -0.1631814734428333746, 0.2012842543237216564, -0.3131151337379057265 ) ) ;
#7377=DIRECTION ( 'NONE',  ( 0.000000000000000000, 0.000000000000000000, 1.000000000000000000 ) ) ;
#7379=EDGE_CURVE ( 'NONE', #13286, #21785, #40091, .T. ) ;
#7409=FACE_OUTER_BOUND ( 'NONE', #19472, .T. ) ;
#7430=ORIENTED_EDGE ( 'NONE', *, *, #40777, .F. ) ;
#7446=ADVANCED_FACE ( 'NONE', ( #39854 ), #22128, .T. ) ;
#7461=CIRCLE ( 'NONE', #34288, 0.2431102362204724532 ) ;
#7462=EDGE_CURVE ( 'NONE', #370, #28768, #69, .T. ) ;
#7490=ORIENTED_EDGE ( 'NONE', *, *, #21276, .T. ) ;
#7516=CARTESIAN_POINT ( 'NONE',  ( -0.1377952755905511306, 1.687505431895958571E-17, -0.3149606299212598381 ) ) ;
#7536=CARTESIAN_POINT ( 'NONE',  ( 0.1574803149606299191, 1.928577636452524918E-17, -0.07924015748031493223 ) ) ;
#7574=CONICAL_SURFACE ( 'NONE', #13695, 0.1574803149606299191, 0.9599310885968713736 ) ;
#7593=LINE ( 'NONE', #37786, #8548 ) ;
#7598=CARTESIAN_POINT ( 'NONE',  ( 0.000000000000000000, 0.000000000000000000, -0.0009999999999999347518 ) ) ;
#7610=FACE_OUTER_BOUND ( 'NONE', #40216, .T. ) ;
#7681=B_SPLINE_CURVE_WITH_KNOTS ( 'NONE', 3,
 ( #12424, #8797, #20054, #23430, #1841, #16480, #38038, #19820, #38510, #3506, #3964, #18581, #29671, #25568, #4418, #7340, #21953, #4188, #43982 ),
 .UNSPECIFIED., .F., .F.,
 ( 4, 2, 2, 1, 2, 2, 2, 2, 2, 4 ),
 ( 0.000000000000000000, 0.2499999999999990563, 0.3749999999999982236, 0.4374999999999977796, 0.4687499999999974465, 0.4999999999999971134, 0.6249999999999972244, 0.6874999999999972244, 0.7499999999999971134, 1.000000000000000000 ),
 .UNSPECIFIED. ) ;
#7692=CARTESIAN_POINT ( 'NONE',  ( 0.1899652659299175261, 0.1858176586719255396, -0.3092881115733999708 ) ) ;
#7714=ORIENTED_EDGE ( 'NONE', *, *, #4187, .T. ) ;
#7721=CARTESIAN_POINT ( 'NONE',  ( -0.05572156214699382215, -0.2633233733571747059, -0.05578523004296883497 ) ) ;
#7734=EDGE_CURVE ( 'NONE', #18573, #28525, #11734, .T. ) ;
#7740=CONICAL_SURFACE ( 'NONE', #9257, 0.1574803149606299191, 0.9599310885968735940 ) ;
#7746=EDGE_CURVE ( 'NONE', #19657, #4309, #1943, .T. ) ;
#7747=DIRECTION ( 'NONE',  ( 0.000000000000000000, 0.000000000000000000, 1.000000000000000000 ) ) ;
#7808=EDGE_CURVE ( 'NONE', #3412, #38506, #1176, .T. ) ;
#7816=CARTESIAN_POINT ( 'NONE',  ( 0.02178664995600260515, -0.2829157040455655414, -0.2993662881637836892 ) ) ;
#7840=CARTESIAN_POINT ( 'NONE',  ( -0.1377952755905512694, 1.687505431895960112E-17, -0.3149606299212598381 ) ) ;
#7858=CARTESIAN_POINT ( 'NONE',  ( 0.2559039420239669349, -0.09551646024251110589, -0.06431648083822334716 ) ) ;
#7860=ORIENTED_EDGE ( 'NONE', *, *, #33079, .T. ) ;
#7876=CARTESIAN_POINT ( 'NONE',  ( 0.000000000000000000, 0.000000000000000000, -0.02633646578327370619 ) ) ;
#7920=VERTEX_POINT ( 'NONE', #34756 ) ;
#7923=ORIENTED_EDGE ( 'NONE', *, *, #23275, .T. ) ;
#7946=CARTESIAN_POINT ( 'NONE',  ( -0.1377952755905511029, 1.687505431895958263E-17, -0.3149606299212598381 ) ) ;
#7966=EDGE_LOOP ( 'NONE', ( #7143, #11533, #18934, #47438 ) ) ;
#7967=CARTESIAN_POINT ( 'NONE',  ( 0.000000000000000000, 0.000000000000000000, -0.1828167807439035619 ) ) ;
#7981=DIRECTION ( 'NONE',  ( 0.5000000000000007772, 0.8660254037844382635, 0.000000000000000000 ) ) ;
#7982=DIRECTION ( 'NONE',  ( -0.8191520442889861364, 1.003171929053517844E-16, 0.5735764363510541530 ) ) ;
#7998=AXIS2_PLACEMENT_3D ( 'NONE', #4350, #41011, #30521 ) ;
#8024=DIRECTION ( 'NONE',  ( 0.000000000000000000, 0.000000000000000000, 1.000000000000000000 ) ) ;
#8066=AXIS2_PLACEMENT_3D ( 'NONE', #6740, #21359, #26633 ) ;
#8097=FACE_OUTER_BOUND ( 'NONE', #21451, .T. ) ;
#8159=EDGE_CURVE ( 'NONE', #30980, #23202, #13030, .T. ) ;
#8222=DIRECTION ( 'NONE',  ( 1.000000000000000000, 0.000000000000000000, 0.000000000000000000 ) ) ;
#8249=CARTESIAN_POINT ( 'NONE',  ( 0.2559055118110236116, 0.1477471161312045311, -0.1122047244094488277 ) ) ;
#8261=VECTOR ( 'NONE', #32210, 39.37007874015748143 ) ;
#8276=DIRECTION ( 'NONE',  ( 0.000000000000000000, 0.000000000000000000, 1.000000000000000000 ) ) ;
#8304=DIRECTION ( 'NONE',  ( 0.000000000000000000, 0.000000000000000000, 1.000000000000000000 ) ) ;
#8326=EDGE_CURVE ( 'NONE', #39783, #20308, #41670, .T. ) ;
#8327=CARTESIAN_POINT ( 'NONE',  ( 0.2559052849838401866, -0.08677120797266399399, -0.05804865129189421685 ) ) ;
#8333=DIRECTION ( 'NONE',  ( 0.000000000000000000, 0.000000000000000000, 1.000000000000000000 ) ) ;
#8339=CONICAL_SURFACE ( 'NONE', #33623, 0.1574803149606299191, 0.9599310885968735940 ) ;
#8341=DIRECTION ( 'NONE',  ( -0.8191520442890001252, 0.000000000000000000, -0.5735764363510340580 ) ) ;
#8373=CARTESIAN_POINT ( 'NONE',  ( -0.03734157890107612371, -0.2739282660277941317, -0.3031249188863139321 ) ) ;
#8411=LINE ( 'NONE', #4813, #12236 ) ;
#8440=AXIS2_PLACEMENT_3D ( 'NONE', #31480, #39108, #6757 ) ;
#8464=DIRECTION ( 'NONE',  ( 1.000000000000000000, 0.000000000000000000, 0.000000000000000000 ) ) ;
#8513=ORIENTED_EDGE ( 'NONE', *, *, #26090, .T. ) ;
#8516=AXIS2_PLACEMENT_3D ( 'NONE', #37232, #26709, #30787 ) ;
#8518=AXIS2_PLACEMENT_3D ( 'NONE', #584, #8024, #44202 ) ;
#8530=CARTESIAN_POINT ( 'NONE',  ( -0.1387979473505290273, -0.2153574986361826149, -0.3148284977848752053 ) ) ;
#8548=VECTOR ( 'NONE', #1103, 39.37007874015748143 ) ;
#8580=CARTESIAN_POINT ( 'NONE',  ( 0.000000000000000000, 0.000000000000000000, -0.1574803149606298636 ) ) ;
#8589=CARTESIAN_POINT ( 'NONE',  ( 0.000000000000000000, 0.000000000000000000, -0.1436967020037460685 ) ) ;
#8598=DIRECTION ( 'NONE',  ( 0.000000000000000000, 0.000000000000000000, 1.000000000000000000 ) ) ;
#8606=VERTEX_POINT ( 'NONE', #8871 ) ;
#8640=VECTOR ( 'NONE', #41032, 39.37007874015748143 ) ;
#8642=CARTESIAN_POINT ( 'NONE',  ( 0.000000000000000000, 0.000000000000000000, -0.3149606299212598381 ) ) ;
#8691=FACE_OUTER_BOUND ( 'NONE', #46644, .T. ) ;
#8755=EDGE_CURVE ( 'NONE', #30017, #38700, #39032, .T. ) ;
#8773=DIRECTION ( 'NONE',  ( 0.000000000000000000, 0.000000000000000000, -1.000000000000000000 ) ) ;
#8797=CARTESIAN_POINT ( 'NONE',  ( -0.2449982982381310737, 0.1540443988236174233, -0.2957398093694128538 ) ) ;
#8803=CARTESIAN_POINT ( 'NONE',  ( 0.2559020992193656863, -0.1090393324022487509, -0.07498935245308939457 ) ) ;
#8807=LINE ( 'NONE', #41369, #19495 ) ;
#8835=CARTESIAN_POINT ( 'NONE',  ( -0.1377952755905509641, 0.000000000000000000, -0.2219368594840610276 ) ) ;
#8871=CARTESIAN_POINT ( 'NONE',  ( -0.1377952755905511861, 1.808041534174241898E-17, -0.09302377043719921301 ) ) ;
#8873=CARTESIAN_POINT ( 'NONE',  ( 0.1279527559055118058, 0.2216206741968047289, -0.3149606299212598381 ) ) ;
#8889=CARTESIAN_POINT ( 'NONE',  ( 2.219626494852212756E-16, 0.2954942322624074524, -0.1122047244094488277 ) ) ;
#8919=CARTESIAN_POINT ( 'NONE',  ( -0.2559055118110236671, -0.1005509620481576105, -0.06804208466526301402 ) ) ;
#8920=B_SPLINE_CURVE_WITH_KNOTS ( 'NONE', 3,
 ( #40662, #15075, #41600, #8803, #16023, #7858, #30193, #8327, #26806, #36866, #19111, #40898, #11715, #27050, #4019, #26088, #33778, #887, #15547, #22476, #41365, #30645, #37092, #33530, #4240 ),
 .UNSPECIFIED., .F., .F.,
 ( 4, 2, 2, 1, 1, 1, 1, 2, 2, 2, 1, 1, 1, 2, 2, 4 ),
 ( 0.000000000000000000, 0.2499999999999949485, 0.3749999999999924505, 0.4374999999999911182, 0.4687499999999905631, 0.4843749999999902855, 0.4921874999999902855, 0.4960937499999901190, 0.4999999999999900080, 0.6249999999999911182, 0.6874999999999916733, 0.7187499999999920064, 0.7343749999999922284, 0.7421874999999924505, 0.7499999999999925615, 1.000000000000000000 ),
 .UNSPECIFIED. ) ;
#8950=CARTESIAN_POINT ( 'NONE',  ( 0.000000000000000000, 0.000000000000000000, 2.731847993664263218E-16 ) ) ;
#8972=CARTESIAN_POINT ( 'NONE',  ( 0.000000000000000000, 0.000000000000000000, -0.2495040853978291451 ) ) ;
#9007=CARTESIAN_POINT ( 'NONE',  ( -0.1832342603886610577, -0.1897030460623687631, -0.3104511204119963508 ) ) ;
#9011=CONICAL_SURFACE ( 'NONE', #26651, 0.1574803149606299191, 0.9599310885968603824 ) ;
#9020=DIRECTION ( 'NONE',  ( 1.000000000000000000, 0.000000000000000000, 0.000000000000000000 ) ) ;
#9039=EDGE_CURVE ( 'NONE', #41713, #8606, #43565, .T. ) ;
#9069=DIRECTION ( 'NONE',  ( 0.8191520442889991260, 1.003171929053533745E-16, -0.5735764363510355013 ) ) ;
#9115=VECTOR ( 'NONE', #27201, 39.37007874015748143 ) ;
#9131=EDGE_LOOP ( 'NONE', ( #37475, #440, #37485, #22892 ) ) ;
#9133=DIRECTION ( 'NONE',  ( 0.8191520442889798082, 0.000000000000000000, 0.5735764363510631458 ) ) ;
#9156=CARTESIAN_POINT ( 'NONE',  ( -0.2559055118110236671, -0.09125550413757829715, -0.06117675834108277783 ) ) ;
#9159=DIRECTION ( 'NONE',  ( 1.000000000000000000, 0.000000000000000000, 0.000000000000000000 ) ) ;
#9170=CONICAL_SURFACE ( 'NONE', #31403, 0.1574803149606299191, 0.9599310885968735940 ) ;
#9190=LINE ( 'NONE', #19500, #9115 ) ;
#9234=CARTESIAN_POINT ( 'NONE',  ( -0.2559055118110236116, -0.1477471161312047254, -0.2921040715117803055 ) ) ;
#9257=AXIS2_PLACEMENT_3D ( 'NONE', #3046, #24877, #43542 ) ;
#9289=ORIENTED_EDGE ( 'NONE', *, *, #15332, .F. ) ;
#9298=LINE ( 'NONE', #23677, #1944 ) ;
#9337=ORIENTED_EDGE ( 'NONE', *, *, #2269, .T. ) ;
#9344=CARTESIAN_POINT ( 'NONE',  ( 0.08209939101888709401, 0.2480946695747454911, -0.3118411609178523558 ) ) ;
#9371=CARTESIAN_POINT ( 'NONE',  ( 0.1030451738609210743, 0.2360010733951117545, -0.03001342526389711579 ) ) ;
#9379=LINE ( 'NONE', #12270, #39265 ) ;
#9385=ORIENTED_EDGE ( 'NONE', *, *, #43935, .F. ) ;
#9414=CARTESIAN_POINT ( 'NONE',  ( -0.09806891812766166394, 0.2388741431483011879, -0.3136338785706627164 ) ) ;
#9418=DIRECTION ( 'NONE',  ( -1.000000000000000000, 0.000000000000000000, 0.000000000000000000 ) ) ;
#9433=DIRECTION ( 'NONE',  ( 1.000000000000000000, 0.000000000000000000, 0.000000000000000000 ) ) ;
#9442=FACE_OUTER_BOUND ( 'NONE', #15304, .T. ) ;
#9452=ORIENTED_EDGE ( 'NONE', *, *, #40711, .F. ) ;
#9467=CARTESIAN_POINT ( 'NONE',  ( 0.2314997995717387735, -0.1618377606623210563, -0.08364281214761010164 ) ) ;
#9476=ORIENTED_EDGE ( 'NONE', *, *, #21119, .T. ) ;
#9505=FACE_OUTER_BOUND ( 'NONE', #42659, .T. ) ;
#9533=DIRECTION ( 'NONE',  ( 0.000000000000000000, 0.000000000000000000, 1.000000000000000000 ) ) ;
#9545=DIRECTION ( 'NONE',  ( 1.000000000000000000, 0.000000000000000000, 0.000000000000000000 ) ) ;
#9597=VECTOR ( 'NONE', #12429, 39.37007874015748143 ) ;
#9611=CARTESIAN_POINT ( 'NONE',  ( 0.1635016310872748624, 0.2010965215412253426, -0.03441347972012011314 ) ) ;
#9659=CARTESIAN_POINT ( 'NONE',  ( 0.2559055118110236116, -0.1477471161312049197, -0.2921040715117803055 ) ) ;
#9698=CARTESIAN_POINT ( 'NONE',  ( 0.2071276943281756266, -0.1759090021854102237, -0.06129781628411451466 ) ) ;
#9713=CARTESIAN_POINT ( 'NONE',  ( -0.2558999865593800660, -0.1227734792635908206, -0.2989668550287328808 ) ) ;
#9720=CARTESIAN_POINT ( 'NONE',  ( -0.1994795808946366045, 0.1803246425350550075, -0.05524818609632883848 ) ) ;
#9736=ORIENTED_EDGE ( 'NONE', *, *, #7462, .T. ) ;
#9740=DIRECTION ( 'NONE',  ( -1.000000000000000000, 0.000000000000000000, 0.000000000000000000 ) ) ;
#9771=DIRECTION ( 'NONE',  ( 0.000000000000000000, 0.000000000000000000, 1.000000000000000000 ) ) ;
#9813=CARTESIAN_POINT ( 'NONE',  ( 0.06073293532416072088, 0.2604299181697357635, -0.3083162604245326399 ) ) ;
#9840=CARTESIAN_POINT ( 'NONE',  ( 0.1017711380106645219, -0.2367366383362172477, -0.03112915705353833454 ) ) ;
#9873=VERTEX_POINT ( 'NONE', #40693 ) ;
#9908=CONICAL_SURFACE ( 'NONE', #22135, 0.1377952755905509363, 0.9599310885968960205 ) ;
#9930=VERTEX_POINT ( 'NONE', #17561 ) ;
#9949=CARTESIAN_POINT ( 'NONE',  ( -0.2011713568916721762, 0.1793478952077579847, -0.05654496252297641634 ) ) ;
#9971=CARTESIAN_POINT ( 'NONE',  ( -0.1377952755905511861, 1.808041534174241898E-17, -0.1321438491773566926 ) ) ;
#9990=DIRECTION ( 'NONE',  ( 0.000000000000000000, 0.000000000000000000, 1.000000000000000000 ) ) ;
#10015=DIRECTION ( 'NONE',  ( 1.000000000000000000, 0.000000000000000000, 0.000000000000000000 ) ) ;
#10041=CARTESIAN_POINT ( 'NONE',  ( 0.1171103306478391837, 0.2278805513379908998, -0.3149606299212597826 ) ) ;
#10050=DIRECTION ( 'NONE',  ( 0.8191520442890534159, 1.003171929053600305E-16, -0.5735764363509581187 ) ) ;
#10057=ORIENTED_EDGE ( 'NONE', *, *, #30937, .T. ) ;
#10064=VECTOR ( 'NONE', #12133, 39.37007874015748143 ) ;
#10069=CARTESIAN_POINT ( 'NONE',  ( 0.1660477163177032645, -0.1996265385480603394, -0.03544556188505140759 ) ) ;
#10071=ADVANCED_FACE ( 'NONE', ( #30221 ), #45660, .F. ) ;
#10072=CARTESIAN_POINT ( 'NONE',  ( 0.1541343738003257691, 0.2065047100574138594, -0.03112915705353490325 ) ) ;
#10088=DIRECTION ( 'NONE',  ( 0.000000000000000000, 0.000000000000000000, 1.000000000000000000 ) ) ;
#10094=DIRECTION ( 'NONE',  ( 1.000000000000000000, 0.000000000000000000, 0.000000000000000000 ) ) ;
#10113=ORIENTED_EDGE ( 'NONE', *, *, #22172, .F. ) ;
#10140=APPLICATION_CONTEXT ( 'automotive_design' ) ;
#10141=ADVANCED_FACE ( 'NONE', ( #38081 ), #31176, .F. ) ;
#10142=CARTESIAN_POINT ( 'NONE',  ( 0.1871882013110628684, -0.1874210200766982803, -0.3098131533094808931 ) ) ;
#10216=CARTESIAN_POINT ( 'NONE',  ( 0.1377952755905509641, 1.687505431895956722E-17, -0.06545654452343109553 ) ) ;
#10237=EDGE_CURVE ( 'NONE', #1846, #26918, #46456, .T. ) ;
#10248=CARTESIAN_POINT ( 'NONE',  ( 0.000000000000000000, 0.000000000000000000, -0.3149606299212598381 ) ) ;
#10292=CARTESIAN_POINT ( 'NONE',  ( 0.2559053792588102949, 0.1035705208482406714, -0.06897712937227379326 ) ) ;
#10298=EDGE_LOOP ( 'NONE', ( #19771, #29545, #36806, #30252 ) ) ;
#10315=CARTESIAN_POINT ( 'NONE',  ( 0.05824109077986203142, -0.2618687228227581376, -0.05388431474956601602 ) ) ;
#10349=AXIS2_PLACEMENT_3D ( 'NONE', #30423, #23674, #38281 ) ;
#10351=ORIENTED_EDGE ( 'NONE', *, *, #11409, .T. ) ;
#10380=AXIS2_PLACEMENT_3D ( 'NONE', #37456, #23326, #18767 ) ;
#10384=CARTESIAN_POINT ( 'NONE',  ( 0.1951724573785894035, -0.1828112239219444324, -0.3083162604244762406 ) ) ;
#10415=EDGE_CURVE ( 'NONE', #41713, #13286, #41853, .T. ) ;
#10424=CARTESIAN_POINT ( 'NONE',  ( 0.2559055118110236116, 0.000000000000000000, -0.3149606299212598381 ) ) ;
#10431=CARTESIAN_POINT ( 'NONE',  ( -0.2460099227178286496, 0.1534603371579498221, -0.09996720075268322736 ) ) ;
#10536=CARTESIAN_POINT ( 'NONE',  ( -0.1377952755905510751, 1.687505431895957647E-17, -0.3149606299212598381 ) ) ;
#10540=EDGE_LOOP ( 'NONE', ( #5002, #23357 ) ) ;
#10557=CARTESIAN_POINT ( 'NONE',  ( 0.09118578515492269110, -0.2428480946569469834, -0.03489849683095880284 ) ) ;
#10646=ORIENTED_EDGE ( 'NONE', *, *, #17959, .F. ) ;
#10655=ORIENTED_EDGE ( 'NONE', *, *, #33529, .T. ) ;
#10658=EDGE_CURVE ( 'NONE', #41311, #14850, #32012, .T. ) ;
#10720=AXIS2_PLACEMENT_3D ( 'NONE', #40829, #14522, #36566 ) ;
#10738=EDGE_CURVE ( 'NONE', #1339, #34984, #46486, .T. ) ;
#10741=EDGE_CURVE ( 'NONE', #65, #38861, #7461, .T. ) ;
#10758=CARTESIAN_POINT ( 'NONE',  ( -0.1574803149606299191, 0.000000000000000000, -0.2748405511811023438 ) ) ;
#10765=FACE_OUTER_BOUND ( 'NONE', #14917, .T. ) ;
#10778=DIRECTION ( 'NONE',  ( 0.000000000000000000, 0.000000000000000000, 1.000000000000000000 ) ) ;
#10827=ORIENTED_EDGE ( 'NONE', *, *, #35976, .T. ) ;
#10832=ORIENTED_EDGE ( 'NONE', *, *, #18438, .F. ) ;
#10835=DIRECTION ( 'NONE',  ( 1.000000000000000000, 0.000000000000000000, 0.000000000000000000 ) ) ;
#10838=CIRCLE ( 'NONE', #16207, 0.1574803149606299191 ) ;
#10881=CARTESIAN_POINT ( 'NONE',  ( -0.06244181591619046151, -0.2594434330345063433, -0.05069326177272678174 ) ) ;
#10917=DIRECTION ( 'NONE',  ( 0.000000000000000000, 0.000000000000000000, 1.000000000000000000 ) ) ;
#10975=CARTESIAN_POINT ( 'NONE',  ( -0.1279527559055118058, 0.2216206741968047289, -0.3149606299212598381 ) ) ;
#11073=AXIS2_PLACEMENT_3D ( 'NONE', #11142, #14261, #43464 ) ;
#11110=EDGE_CURVE ( 'NONE', #18657, #23237, #11395, .T. ) ;
#11112=CARTESIAN_POINT ( 'NONE',  ( -0.2360031691064421178, -0.1592377390491987732, -0.08759220388363096743 ) ) ;
#11142=CARTESIAN_POINT ( 'NONE',  ( 0.000000000000000000, 0.000000000000000000, -0.3001770169643759867 ) ) ;
#11179=EDGE_CURVE ( 'NONE', #4869, #23841, #37321, .T. ) ;
#11194=EDGE_LOOP ( 'NONE', ( #31584, #40026, #5957, #2102 ) ) ;
#11202=CARTESIAN_POINT ( 'NONE',  ( 0.06453057165843432974, -0.2582375021999246956, -0.3090319486758518197 ) ) ;
#11239=DIRECTION ( 'NONE',  ( 0.000000000000000000, 0.000000000000000000, 1.000000000000000000 ) ) ;
#11262=CARTESIAN_POINT ( 'NONE',  ( -0.1574803149606299191, 1.928577636452524610E-17, -0.3149606299212598381 ) ) ;
#11268=DIRECTION ( 'NONE',  ( 1.000000000000000000, 0.000000000000000000, 0.000000000000000000 ) ) ;
#11340=CARTESIAN_POINT ( 'NONE',  ( -0.2170082705494138786, -0.1702044488443286430, -0.06846571731941632211 ) ) ;
#11357=ORIENTED_EDGE ( 'NONE', *, *, #33834, .T. ) ;
#11395=LINE ( 'NONE', #15234, #20472 ) ;
#11408=CARTESIAN_POINT ( 'NONE',  ( -0.2559055118110236116, -0.08227967500866986694, -0.05504294401599051090 ) ) ;
#11409=EDGE_CURVE ( 'NONE', #954, #25562, #2933, .T. ) ;
#11435=ADVANCED_FACE ( 'NONE', ( #25500 ), #46520, .F. ) ;
#11459=FACE_OUTER_BOUND ( 'NONE', #32987, .T. ) ;
#11473=AXIS2_PLACEMENT_3D ( 'NONE', #20398, #35037, #12537 ) ;
#11522=DIRECTION ( 'NONE',  ( 0.000000000000000000, 0.000000000000000000, 1.000000000000000000 ) ) ;
#11525=ORIENTED_EDGE ( 'NONE', *, *, #29179, .F. ) ;
#11531=EDGE_LOOP ( 'NONE', ( #45257, #30073, #25689, #40926 ) ) ;
#11533=ORIENTED_EDGE ( 'NONE', *, *, #9039, .T. ) ;
#11667=LINE ( 'NONE', #1800, #10064 ) ;
#11682=VECTOR ( 'NONE', #22981, 39.37007874015748143 ) ;
#11684=CARTESIAN_POINT ( 'NONE',  ( 0.1574803149606299191, 1.928577636452524610E-17, -0.1183602362204724257 ) ) ;
#11715=CARTESIAN_POINT ( 'NONE',  ( 0.2559055130920101506, -0.08227836217959635934, -0.05504206144341895063 ) ) ;
#11734=B_SPLINE_CURVE_WITH_KNOTS ( 'NONE', 3,
 ( #45805, #13013, #37695, #27656, #42210, #4848, #9414, #24033, #38637, #30774, #16374, #5809, #1253, #30999, #34126, #30531, #45092 ),
 .UNSPECIFIED., .F., .F.,
 ( 4, 2, 2, 2, 2, 1, 2, 2, 4 ),
 ( 0.000000000000000000, 0.1250000000000007216, 0.1875000000000010825, 0.2500000000000014433, 0.3750000000000018319, 0.4375000000000019984, 0.4687500000000020539, 0.5000000000000019984, 1.000000000000000000 ),
 .UNSPECIFIED. ) ;
#11779=CARTESIAN_POINT ( 'NONE',  ( -0.2559086337351289542, 0.02188737959670186695, -0.3144303560290073740 ) ) ;
#11802=CARTESIAN_POINT ( 'NONE',  ( 0.1377952755905511861, 0.000000000000000000, -0.2495040853978291451 ) ) ;
#11813=DIRECTION ( 'NONE',  ( 1.000000000000000000, 0.000000000000000000, 0.000000000000000000 ) ) ;
#11816=ORIENTED_EDGE ( 'NONE', *, *, #16723, .T. ) ;
#11822=ADVANCED_FACE ( 'NONE', ( #6718 ), #9011, .F. ) ;
#11833=DIRECTION ( 'NONE',  ( -0.8191520442889996811, 0.000000000000000000, -0.5735764363510347241 ) ) ;
#11845=CARTESIAN_POINT ( 'NONE',  ( 0.000000000000000000, 0.000000000000000000, -0.2103840066576717072 ) ) ;
#11857=DIRECTION ( 'NONE',  ( 1.000000000000000000, 0.000000000000000000, 0.000000000000000000 ) ) ;
#11921=CARTESIAN_POINT ( 'NONE',  ( 0.1574803149606299191, 0.000000000000000000, -0.1966003937007873570 ) ) ;
#11925=CONICAL_SURFACE ( 'NONE', #44800, 0.1574803149606299191, 0.9599310885968735940 ) ;
#12012=ORIENTED_EDGE ( 'NONE', *, *, #17959, .T. ) ;
#12027=CARTESIAN_POINT ( 'NONE',  ( 0.05642593091638736097, 0.2629167058585549221, -0.05524818609632992789 ) ) ;
#12075=SHAPE_DEFINITION_REPRESENTATION ( #42283, #1042 ) ;
#12090=EDGE_CURVE ( 'NONE', #28525, #43008, #42147, .T. ) ;
#12125=DIRECTION ( 'NONE',  ( 1.000000000000000000, 0.000000000000000000, 0.000000000000000000 ) ) ;
#12133=DIRECTION ( 'NONE',  ( 0.8191520442889861364, 0.000000000000000000, 0.5735764363510541530 ) ) ;
#12230=CARTESIAN_POINT ( 'NONE',  ( -0.05036568513382595758, -0.2664124483477782190, -0.3061783854718737596 ) ) ;
#12236=VECTOR ( 'NONE', #33617, 39.37007874015748854 ) ;
#12261=CARTESIAN_POINT ( 'NONE',  ( 0.05473415491935430810, 0.2638934531858505017, -0.05654496252297439018 ) ) ;
#12270=CARTESIAN_POINT ( 'NONE',  ( 0.1574803149606299191, 0.000000000000000000, 2.731847993664263218E-16 ) ) ;
#12307=CARTESIAN_POINT ( 'NONE',  ( -0.2559070959273828105, 0.05936816977299741449, -0.3110460671459447379 ) ) ;
#12354=DIRECTION ( 'NONE',  ( 1.000000000000000000, 0.000000000000000000, 0.000000000000000000 ) ) ;
#12358=ORIENTED_EDGE ( 'NONE', *, *, #25512, .F. ) ;
#12376=CARTESIAN_POINT ( 'NONE',  ( -0.2559082480989984254, -0.02481004614261094615, -0.3144388117053942833 ) ) ;
#12378=CIRCLE ( 'NONE', #8516, 0.1574803149606299191 ) ;
#12417=ORIENTED_EDGE ( 'NONE', *, *, #27367, .F. ) ;
#12424=CARTESIAN_POINT ( 'NONE',  ( -0.2559055118110236116, 0.1477471161312047254, -0.2921040715117803055 ) ) ;
#12429=DIRECTION ( 'NONE',  ( 0.000000000000000000, 0.000000000000000000, 1.000000000000000000 ) ) ;
#12437=CONICAL_SURFACE ( 'NONE', #43778, 0.1377952755905509641, 0.9599310885968941331 ) ;
#12440=ADVANCED_BREP_SHAPE_REPRESENTATION ( 'ISO 10513 M8 Lock Nut', ( #4462, #20860 ), #17833 ) ;
#12445=CYLINDRICAL_SURFACE ( 'NONE', #19300, 0.1377952755905510751 ) ;
#12463=EDGE_LOOP ( 'NONE', ( #9289, #39728 ) ) ;
#12473=ORIENTED_EDGE ( 'NONE', *, *, #24133, .F. ) ;
#12482=CARTESIAN_POINT ( 'NONE',  ( 0.04256392708710985545, 0.2709142457700762230, -0.3044102143378303871 ) ) ;
#12537=DIRECTION ( 'NONE',  ( 1.000000000000000000, 0.000000000000000000, 0.000000000000000000 ) ) ;
#12543=ORIENTED_EDGE ( 'NONE', *, *, #43810, .T. ) ;
#12569=ORIENTED_EDGE ( 'NONE', *, *, #3461, .T. ) ;
#12631=CARTESIAN_POINT ( 'NONE',  ( -0.1496320939564846353, -0.2091027599427721095, -0.3142669362052405435 ) ) ;
#12654=EDGE_LOOP ( 'NONE', ( #7337, #32767, #13334, #30925 ) ) ;
#12671=DIRECTION ( 'NONE',  ( -0.000000000000000000, -0.000000000000000000, -1.000000000000000000 ) ) ;
#12688=VECTOR ( 'NONE', #16262, 39.37007874015748143 ) ;
#12747=CARTESIAN_POINT ( 'NONE',  ( 0.1987795079023654821, 0.1807288298655941872, -0.05471869868084587585 ) ) ;
#12772=CARTESIAN_POINT ( 'NONE',  ( -0.2559055118110236116, -0.02858058760286992517, -0.02996975140571705304 ) ) ;
#12788=EDGE_CURVE ( 'NONE', #25178, #16859, #42725, .T. ) ;
#12810=CARTESIAN_POINT ( 'NONE',  ( -0.1574803149606299191, 1.928577636452524610E-17, -0.04012007874015743186 ) ) ;
#12827=CARTESIAN_POINT ( 'NONE',  ( 0.1387979473508932082, 0.2153574986359478305, -0.3148284977848753163 ) ) ;
#12844=ORIENTED_EDGE ( 'NONE', *, *, #30294, .T. ) ;
#12945=ORIENTED_EDGE ( 'NONE', *, *, #2957, .T. ) ;
#12974=CARTESIAN_POINT ( 'NONE',  ( 0.1789895911305919018, 0.1921545436410181107, -0.04147023971056211511 ) ) ;
#13013=CARTESIAN_POINT ( 'NONE',  ( -0.1225179410722563866, 0.2247584660037810489, -0.3149606299212600047 ) ) ;
#13017=CARTESIAN_POINT ( 'NONE',  ( 0.000000000000000000, 0.000000000000000000, -0.06545654452343109553 ) ) ;
#13030=B_SPLINE_CURVE_WITH_KNOTS ( 'NONE', 3,
 ( #22169, #30519, #23307, #8919, #9156, #23066, #23547, #3959, #44208, #19698, #11408, #36807, #34113, #26026, #36573, #120, #34565, #37684, #45552, #12772, #15896, #37924 ),
 .UNSPECIFIED., .F., .F.,
 ( 4, 1, 1, 1, 1, 1, 1, 2, 2, 1, 1, 1, 1, 2, 2, 4 ),
 ( 0.000000000000000000, 0.2499999999999965028, 0.3749999999999947820, 0.4374999999999938938, 0.4687499999999934497, 0.4843749999999932276, 0.4921874999999932832, 0.4960937499999931721, 0.4999999999999930056, 0.6249999999999954481, 0.6874999999999966693, 0.7187499999999973355, 0.7343749999999976685, 0.7421874999999977796, 0.7499999999999978906, 1.000000000000000000 ),
 .UNSPECIFIED. ) ;
#13040=CARTESIAN_POINT ( 'NONE',  ( 0.000000000000000000, 0.000000000000000000, -0.3149606299212598381 ) ) ;
#13067=DIRECTION ( 'NONE',  ( -0.5000000000000003331, 0.8660254037844384856, 0.000000000000000000 ) ) ;
#13084=ORIENTED_EDGE ( 'NONE', *, *, #29179, .T. ) ;
#13110=ORIENTED_EDGE ( 'NONE', *, *, #3191, .F. ) ;
#13126=ORIENTED_EDGE ( 'NONE', *, *, #16477, .T. ) ;
#13140=DIRECTION ( 'NONE',  ( 1.000000000000000000, 0.000000000000000000, 0.000000000000000000 ) ) ;
#13146=CARTESIAN_POINT ( 'NONE',  ( 0.000000000000000000, 0.000000000000000000, -0.3149606299212598381 ) ) ;
#13168=EDGE_LOOP ( 'NONE', ( #5004, #40027, #37328, #45512 ) ) ;
#13192=CARTESIAN_POINT ( 'NONE',  ( 0.2559035040615164069, 0.02868498164184919361, -0.03078275702940447625 ) ) ;
#13209=AXIS2_PLACEMENT_3D ( 'NONE', #36601, #36379, #36836 ) ;
#13235=DIRECTION ( 'NONE',  ( 1.000000000000000000, 0.000000000000000000, 0.000000000000000000 ) ) ;
#13261=CONICAL_SURFACE ( 'NONE', #35467, 0.1377952755905510751, 0.9599310885968951323 ) ;
#13286=VERTEX_POINT ( 'NONE', #4721 ) ;
#13293=CARTESIAN_POINT ( 'NONE',  ( 0.000000000000000000, 0.000000000000000000, -0.07924015748031493223 ) ) ;
#13305=AXIS2_PLACEMENT_3D ( 'NONE', #32421, #28591, #32891 ) ;
#13319=FACE_OUTER_BOUND ( 'NONE', #5249, .T. ) ;
#13334=ORIENTED_EDGE ( 'NONE', *, *, #27094, .F. ) ;
#13355=CIRCLE ( 'NONE', #41667, 0.1377952755905510751 ) ;
#13377=ADVANCED_FACE ( 'NONE', ( #32039 ), #31811, .F. ) ;
#13418=CARTESIAN_POINT ( 'NONE',  ( 0.2559055147610055925, 0.04268399720878558040, -0.03497896297209982658 ) ) ;
#13424=EDGE_LOOP ( 'NONE', ( #22046, #36975, #3266, #32673 ) ) ;
#13443=VERTEX_POINT ( 'NONE', #46398 ) ;
#13462=ORIENTED_EDGE ( 'NONE', *, *, #7734, .T. ) ;
#13471=ORIENTED_EDGE ( 'NONE', *, *, #37378, .F. ) ;
#13475=CONICAL_SURFACE ( 'NONE', #15818, 0.1377952755905510196, 0.9599310885968940221 ) ;
#13485=CARTESIAN_POINT ( 'NONE',  ( 0.2559055118110235560, -0.1161062301479638820, -0.3006843207781718097 ) ) ;
#13539=CARTESIAN_POINT ( 'NONE',  ( -0.05949606008255010903, 0.2611441659580247543, -0.05295753290290025617 ) ) ;
#13558=ORIENTED_EDGE ( 'NONE', *, *, #46516, .F. ) ;
#13596=CARTESIAN_POINT ( 'NONE',  ( -0.2559055118110235560, 0.01785997614104697234, -0.02837153189565116279 ) ) ;
#13617=CARTESIAN_POINT ( 'NONE',  ( 0.000000000000000000, 0.000000000000000000, -0.3149606299212598381 ) ) ;
#13651=FACE_OUTER_BOUND ( 'NONE', #45015, .T. ) ;
#13659=CARTESIAN_POINT ( 'NONE',  ( 0.1154865254643520911, 0.2288180556977880420, -0.02742975588280811144 ) ) ;
#13667=EDGE_LOOP ( 'NONE', ( #11357, #46208, #10113, #2249 ) ) ;
#13695=AXIS2_PLACEMENT_3D ( 'NONE', #41580, #24127, #9020 ) ;
#13758=EDGE_LOOP ( 'NONE', ( #45992, #34616, #19268, #17011 ) ) ;
#13827=AXIS2_PLACEMENT_3D ( 'NONE', #5591, #16844, #41749 ) ;
#13836=FACE_OUTER_BOUND ( 'NONE', #40267, .T. ) ;
#13849=FACE_OUTER_BOUND ( 'NONE', #17685, .T. ) ;
#13915=FACE_OUTER_BOUND ( 'NONE', #19759, .T. ) ;
#13922=ADVANCED_FACE ( 'NONE', ( #5380 ), #17586, .F. ) ;
#13948=CARTESIAN_POINT ( 'NONE',  ( 0.2559055118110236116, -0.1349029091040385986, -0.2958118747041117436 ) ) ;
#13991=CARTESIAN_POINT ( 'NONE',  ( 0.1997612633124547232, -0.1801620131153035542, -0.05546260682012722071 ) ) ;
#14013=CARTESIAN_POINT ( 'NONE',  ( -0.07691592068040527252, 0.2510868047526074176, -0.04147023971058640124 ) ) ;
#14072=DIRECTION ( 'NONE',  ( -1.000000000000000000, 0.000000000000000000, 0.000000000000000000 ) ) ;
#14119=CARTESIAN_POINT ( 'NONE',  ( 0.2559055093128127512, 0.08129821535987498404, -0.05440291541350525395 ) ) ;
#14141=CONICAL_SURFACE ( 'NONE', #11073, 0.1377952755905513804, 0.9599310885968808105 ) ;
#14167=DIRECTION ( 'NONE',  ( 0.000000000000000000, 0.000000000000000000, 1.000000000000000000 ) ) ;
#14181=VECTOR ( 'NONE', #35040, 39.37007874015748143 ) ;
#14187=CARTESIAN_POINT ( 'NONE',  ( 0.000000000000000000, 0.000000000000000000, -0.05390369169704170571 ) ) ;
#14215=CARTESIAN_POINT ( 'NONE',  ( -0.1377952755905511861, 1.808041534174241898E-17, -0.2103840066576717072 ) ) ;
#14222=ORIENTED_EDGE ( 'NONE', *, *, #29050, .F. ) ;
#14251=VECTOR ( 'NONE', #38645, 39.37007874015748143 ) ;
#14261=DIRECTION ( 'NONE',  ( -0.000000000000000000, -0.000000000000000000, -1.000000000000000000 ) ) ;
#14286=ORIENTED_EDGE ( 'NONE', *, *, #46789, .F. ) ;
#14288=EDGE_LOOP ( 'NONE', ( #36070, #40206, #44846, #15358, #44675, #222, #2725 ) ) ;
#14310=ORIENTED_EDGE ( 'NONE', *, *, #41954, .F. ) ;
#14320=DIRECTION ( 'NONE',  ( 0.000000000000000000, 0.000000000000000000, 1.000000000000000000 ) ) ;
#14326=CARTESIAN_POINT ( 'NONE',  ( -0.2559055118110235560, 0.1029525201786305882, -0.06857031309820646459 ) ) ;
#14336=ORIENTED_EDGE ( 'NONE', *, *, #22172, .T. ) ;
#14418=ORIENTED_EDGE ( 'NONE', *, *, #43208, .T. ) ;
#14426=DIRECTION ( 'NONE',  ( -1.000000000000000000, 0.000000000000000000, 0.000000000000000000 ) ) ;
#14436=CARTESIAN_POINT ( 'NONE',  ( 0.000000000000000000, 0.000000000000000000, -0.3149606299212598381 ) ) ;
#14441=DIRECTION ( 'NONE',  ( 0.000000000000000000, 0.000000000000000000, 1.000000000000000000 ) ) ;
#14459=CARTESIAN_POINT ( 'NONE',  ( -0.1030451738610134865, -0.2360010733950600459, -0.03001342526388867810 ) ) ;
#14516=CARTESIAN_POINT ( 'NONE',  ( 0.000000000000000000, 0.000000000000000000, -0.1045766232635885612 ) ) ;
#14522=DIRECTION ( 'NONE',  ( 0.000000000000000000, 0.000000000000000000, 1.000000000000000000 ) ) ;
#14568=CARTESIAN_POINT ( 'NONE',  ( 0.000000000000000000, 0.000000000000000000, -0.3149606299212598381 ) ) ;
#14594=ORIENTED_EDGE ( 'NONE', *, *, #33207, .F. ) ;
#14610=ADVANCED_FACE ( 'NONE', ( #10765 ), #9908, .F. ) ;
#14650=AXIS2_PLACEMENT_3D ( 'NONE', #23341, #38176, #19959 ) ;
#14651=ORIENTED_EDGE ( 'NONE', *, *, #10658, .T. ) ;
#14652=ORIENTED_EDGE ( 'NONE', *, *, #21097, .F. ) ;
#14654=VECTOR ( 'NONE', #6122, 39.37007874015748143 ) ;
#14687=ORIENTED_EDGE ( 'NONE', *, *, #45544, .F. ) ;
#14786=B_SPLINE_CURVE_WITH_KNOTS ( 'NONE', 3,
 ( #2041, #10431, #5643, #21186, #38714, #31773, #9949, #28410, #20254, #9720, #24797, #5884, #20491, #46589, #2275, #16901, #35362, #31541, #34901, #27727, #39390, #42289, #24334, #35819, #17601, #27950, #6094, #2966, #32244, #46825, #14013, #28660, #17131, #13539, #42734, #24558, #29857, #32724, #22375, #36538, #43944 ),
 .UNSPECIFIED., .F., .F.,
 ( 4, 1, 1, 1, 1, 1, 1, 2, 2, 1, 1, 1, 1, 2, 2, 2, 1, 1, 1, 1, 2, 2, 1, 1, 1, 1, 1, 2, 2, 4 ),
 ( 0.000000000000000000, 0.1249999999999970579, 0.1874999999999955869, 0.2187499999999950318, 0.2343749999999947820, 0.2421874999999946987, 0.2460937499999945599, 0.2480468749999945044, 0.2499999999999944489, 0.3124999999999964473, 0.3437499999999976685, 0.3593749999999985012, 0.3671874999999988343, 0.3710937499999988343, 0.3749999999999987788, 0.5000000000000011102, 0.5625000000000022204, 0.5937500000000027756, 0.6093750000000029976, 0.6171875000000029976, 0.6210937500000028866, 0.6250000000000027756, 0.6875000000000015543, 0.7187500000000008882, 0.7343750000000005551, 0.7421875000000004441, 0.7460937500000003331, 0.7480468750000002220, 0.7500000000000002220, 1.000000000000000000 ),
 .UNSPECIFIED. ) ;
#14795=PRODUCT_DEFINITION_FORMATION_WITH_SPECIFIED_SOURCE ( 'ANY', '', #5552, .NOT_KNOWN. ) ;
#14829=AXIS2_PLACEMENT_3D ( 'NONE', #21068, #39511, #35248 ) ;
#14850=VERTEX_POINT ( 'NONE', #22940 ) ;
#14854=LINE ( 'NONE', #11262, #37345 ) ;
#14868=CARTESIAN_POINT ( 'NONE',  ( 0.000000000000000000, 0.000000000000000000, -0.2495040853978291451 ) ) ;
#14892=ADVANCED_FACE ( 'NONE', ( #20226 ), #16651, .T. ) ;
#14893=ORIENTED_EDGE ( 'NONE', *, *, #22956, .F. ) ;
#14905=CLOSED_SHELL ( 'NONE', ( #33615, #13922, #10071, #4201, #15721, #35465, #34519, #13377, #40384, #39122, #42178, #17365, #14610, #23948, #43223, #18007, #22947, #35019, #42758, #2585, #31351, #24312, #25352, #30250, #42349, #24315, #25675, #4349, #839, #21593, #36484, #19761, #5302, #36719, #31933, #19807, #18602, #15115, #6098, #38307, #7446, #14892, #40453, #15165, #11822, #23753, #28944, #6703, #2065, #1184, #24951, #11435, #22190, #41607, #23990, #23507, #30061, #31618, #632, #42563, #5567, #10141, #19475, #23811, #16464, #26039, #5992, #2737, #28710, #26277 ) ) ;
#14917=EDGE_LOOP ( 'NONE', ( #28213, #4260, #34643, #12358 ) ) ;
#14937=CARTESIAN_POINT ( 'NONE',  ( 0.000000000000000000, 0.000000000000000000, -0.06545654452343109553 ) ) ;
#14938=CARTESIAN_POINT ( 'NONE',  ( -0.1889095778403545312, -0.1864272366437806083, -0.04769437235514253220 ) ) ;
#14958=ORIENTED_EDGE ( 'NONE', *, *, #45634, .F. ) ;
#14968=CONICAL_SURFACE ( 'NONE', #15762, 0.1377952755905509641, 0.9599310885968941331 ) ;
#14981=LINE ( 'NONE', #36543, #29810 ) ;
#15039=AXIS2_PLACEMENT_3D ( 'NONE', #32822, #10778, #25851 ) ;
#15075=CARTESIAN_POINT ( 'NONE',  ( 0.2559055118110236671, -0.1364700349299463877, -0.1001271636663048775 ) ) ;
#15115=ADVANCED_FACE ( 'NONE', ( #30514 ), #37919, .T. ) ;
#15150=CARTESIAN_POINT ( 'NONE',  ( 0.05572156214699040822, 0.2633233733571749835, -0.05578523004296867538 ) ) ;
#15157=EDGE_CURVE ( 'NONE', #954, #6423, #4541, .T. ) ;
#15165=ADVANCED_FACE ( 'NONE', ( #18977 ), #999, .F. ) ;
#15186=VERTEX_POINT ( 'NONE', #2415 ) ;
#15234=CARTESIAN_POINT ( 'NONE',  ( -0.1574803149606299191, 1.928577636452524610E-17, -0.0009999999999999347518 ) ) ;
#15282=FACE_OUTER_BOUND ( 'NONE', #4913, .T. ) ;
#15304=EDGE_LOOP ( 'NONE', ( #32357, #24069, #10655, #33477 ) ) ;
#15319=DIRECTION ( 'NONE',  ( 1.000000000000000000, 0.000000000000000000, 0.000000000000000000 ) ) ;
#15324=DIRECTION ( 'NONE',  ( 0.000000000000000000, 0.000000000000000000, 1.000000000000000000 ) ) ;
#15332=EDGE_CURVE ( 'NONE', #26580, #24404, #3039, .T. ) ;
#15358=ORIENTED_EDGE ( 'NONE', *, *, #37069, .F. ) ;
#15366=EDGE_CURVE ( 'NONE', #45855, #21785, #20631, .T. ) ;
#15438=CIRCLE ( 'NONE', #35324, 0.2559055118110236116 ) ;
#15496=CIRCLE ( 'NONE', #13209, 0.2431102362204724532 ) ;
#15528=ORIENTED_EDGE ( 'NONE', *, *, #39349, .T. ) ;
#15547=CARTESIAN_POINT ( 'NONE',  ( 0.2559054473914413874, -0.04584745133446761767, -0.03612980868771894366 ) ) ;
#15558=AXIS2_PLACEMENT_3D ( 'NONE', #38599, #5058, #5532 ) ;
#15602=CARTESIAN_POINT ( 'NONE',  ( 0.000000000000000000, 0.000000000000000000, -0.3149606299212598381 ) ) ;
#15610=CARTESIAN_POINT ( 'NONE',  ( -0.2559125663627066505, 0.04383012413643278676, -0.3128473781736403891 ) ) ;
#15626=CARTESIAN_POINT ( 'NONE',  ( 0.04075098337900059237, 0.2719666410387984179, -0.06815351164857791355 ) ) ;
#15642=EDGE_LOOP ( 'NONE', ( #19926, #29287, #34158, #37432 ) ) ;
#15669=CARTESIAN_POINT ( 'NONE',  ( -0.2559061023261890999, 0.06403729604667574016, -0.3104221027878572570 ) ) ;
#15682=VERTEX_POINT ( 'NONE', #697 ) ;
#15701=CARTESIAN_POINT ( 'NONE',  ( -0.1567662409572586624, 1.924205194239609999E-17, -0.0004999999999998990712 ) ) ;
#15721=ADVANCED_FACE ( 'NONE', ( #33347 ), #26861, .F. ) ;
#15752=CARTESIAN_POINT ( 'NONE',  ( -0.1377952755905511861, 1.808041534174241898E-17, -0.2886241641379866385 ) ) ;
#15762=AXIS2_PLACEMENT_3D ( 'NONE', #13017, #42215, #9418 ) ;
#15763=AXIS2_PLACEMENT_3D ( 'NONE', #32289, #39438, #35857 ) ;
#15796=DIRECTION ( 'NONE',  ( 0.000000000000000000, 0.000000000000000000, 1.000000000000000000 ) ) ;
#15810=CARTESIAN_POINT ( 'NONE',  ( -0.2559055118110236116, -0.1477471161312047254, -0.2921040715117803055 ) ) ;
#15815=ORIENTED_EDGE ( 'NONE', *, *, #6602, .T. ) ;
#15818=AXIS2_PLACEMENT_3D ( 'NONE', #22649, #3946, #23124 ) ;
#15835=ORIENTED_EDGE ( 'NONE', *, *, #3757, .T. ) ;
#15837=CARTESIAN_POINT ( 'NONE',  ( -0.1574803149606299191, 1.928577636452524610E-17, -0.2748405511811023438 ) ) ;
#15869=DIRECTION ( 'NONE',  ( 1.000000000000000000, 0.000000000000000000, 0.000000000000000000 ) ) ;
#15896=CARTESIAN_POINT ( 'NONE',  ( -0.2559055118110236671, -0.01424369123639110390, -0.02740704184215039807 ) ) ;
#15920=DIRECTION ( 'NONE',  ( 1.000000000000000000, 0.000000000000000000, 0.000000000000000000 ) ) ;
#15933=DIRECTION ( 'NONE',  ( 0.000000000000000000, 0.000000000000000000, 1.000000000000000000 ) ) ;
#15934=DIRECTION ( 'NONE',  ( 0.000000000000000000, 0.000000000000000000, 1.000000000000000000 ) ) ;
#15953=B_SPLINE_CURVE_WITH_KNOTS ( 'NONE', 3,
 ( #17344, #35573, #9467, #28390, #9698, #2483, #24774, #2942, #13991, #20469, #35105, #2251, #35254, #46236, #6933, #20609, #43587, #10069, #28787, #6218, #20843, #28541, #39283, #9840, #35484, #21075, #2849, #46475, #10557, #6458, #36193, #39519, #35713, #47201, #10315, #2623, #31894, #17726, #17487, #17024, #38825 ),
 .UNSPECIFIED., .F., .F.,
 ( 4, 1, 1, 1, 1, 1, 1, 2, 2, 1, 1, 1, 1, 2, 2, 2, 1, 1, 1, 1, 2, 2, 1, 1, 1, 1, 1, 2, 2, 4 ),
 ( 0.000000000000000000, 0.1250000000000026368, 0.1875000000000038303, 0.2187500000000044131, 0.2343750000000046352, 0.2421875000000046629, 0.2460937500000047740, 0.2480468750000047462, 0.2500000000000046629, 0.3125000000000010547, 0.3437499999999993894, 0.3593749999999987232, 0.3671874999999983347, 0.3710937499999981681, 0.3749999999999980016, 0.4999999999999946709, 0.5624999999999930056, 0.5937499999999921174, 0.6093749999999916733, 0.6171874999999913403, 0.6210937499999912292, 0.6249999999999911182, 0.6874999999999893419, 0.7187499999999884537, 0.7343749999999880096, 0.7421874999999876765, 0.7460937499999875655, 0.7480468749999874545, 0.7499999999999873435, 1.000000000000000000 ),
 .UNSPECIFIED. ) ;
#15973=CARTESIAN_POINT ( 'NONE',  ( 0.000000000000000000, 0.000000000000000000, -0.3139606299212599483 ) ) ;
#15974=AXIS2_PLACEMENT_3D ( 'NONE', #39230, #16968, #2568 ) ;
#15986=CARTESIAN_POINT ( 'NONE',  ( -0.1658511544270574734, -0.1997399692762479584, -0.3128573757128095267 ) ) ;
#16002=CARTESIAN_POINT ( 'NONE',  ( 0.1574803149606299191, 1.928577636452524918E-17, -0.0009999999999999347518 ) ) ;
#16014=DIRECTION ( 'NONE',  ( 1.000000000000000000, 0.000000000000000000, 0.000000000000000000 ) ) ;
#16023=CARTESIAN_POINT ( 'NONE',  ( 0.2559026586320093388, -0.1036163276257849458, -0.07053060040796885199 ) ) ;
#16030=AXIS2_PLACEMENT_3D ( 'NONE', #13040, #28616, #20678 ) ;
#16111=ORIENTED_EDGE ( 'NONE', *, *, #46727, .F. ) ;
#16118=DIRECTION ( 'NONE',  ( 0.8191520442889991260, 1.003171929053533745E-16, -0.5735764363510355013 ) ) ;
#16182=CARTESIAN_POINT ( 'NONE',  ( 0.1377952755905510474, 0.000000000000000000, -0.2610569382242185488 ) ) ;
#16206=VECTOR ( 'NONE', #8276, 39.37007874015748143 ) ;
#16207=AXIS2_PLACEMENT_3D ( 'NONE', #16586, #35508, #10094 ) ;
#16246=ORIENTED_EDGE ( 'NONE', *, *, #6215, .F. ) ;
#16259=VECTOR ( 'NONE', #3872, 39.37007874015748143 ) ;
#16262=DIRECTION ( 'NONE',  ( 0.000000000000000000, 0.000000000000000000, 1.000000000000000000 ) ) ;
#16336=CARTESIAN_POINT ( 'NONE',  ( 0.06244181591614397786, 0.2594434330345316564, -0.05069326177275422507 ) ) ;
#16342=DIRECTION ( 'NONE',  ( 0.000000000000000000, 0.000000000000000000, 1.000000000000000000 ) ) ;
#16374=CARTESIAN_POINT ( 'NONE',  ( -0.07267052686971341158, 0.2535370473722451390, -0.3104511204117335610 ) ) ;
#16379=MECHANICAL_DESIGN_GEOMETRIC_PRESENTATION_REPRESENTATION('',(#3365),#43888);
#16413=EDGE_CURVE ( 'NONE', #19150, #17741, #26056, .T. ) ;
#16464=ADVANCED_FACE ( 'NONE', ( #1358 ), #31432, .F. ) ;
#16473=AXIS2_PLACEMENT_3D ( 'NONE', #21237, #43514, #24376 ) ;
#16477=EDGE_CURVE ( 'NONE', #31750, #18573, #7681, .T. ) ;
#16480=CARTESIAN_POINT ( 'NONE',  ( -0.2055371055870141295, 0.1768241869786838227, -0.3061783854717646802 ) ) ;
#16559=CARTESIAN_POINT ( 'NONE',  ( 0.1889095778402860304, 0.1864272366438185224, -0.04769437235510193968 ) ) ;
#16562=ORIENTED_EDGE ( 'NONE', *, *, #7808, .F. ) ;
#16566=CARTESIAN_POINT ( 'NONE',  ( 0.000000000000000000, 0.000000000000000000, -0.1045766232635885612 ) ) ;
#16576=CARTESIAN_POINT ( 'NONE',  ( -0.1377952755905510474, 1.687505431895957955E-17, -0.2610569382242185488 ) ) ;
#16586=CARTESIAN_POINT ( 'NONE',  ( 0.000000000000000000, 0.000000000000000000, -0.3149606299212598381 ) ) ;
#16651=PLANE ( 'NONE',  #734 ) ;
#16658=DIRECTION ( 'NONE',  ( 1.000000000000000000, 0.000000000000000000, 0.000000000000000000 ) ) ;
#16664=CARTESIAN_POINT ( 'NONE',  ( -0.2559055118110236116, 0.000000000000000000, -0.3149606299212598381 ) ) ;
#16669=EDGE_CURVE ( 'NONE', #24988, #2951, #24317, .T. ) ;
#16715=FACE_OUTER_BOUND ( 'NONE', #43871, .T. ) ;
#16719=VERTEX_POINT ( 'NONE', #24087 ) ;
#16722=LINE ( 'NONE', #42564, #12688 ) ;
#16723=EDGE_CURVE ( 'NONE', #15186, #2951, #19164, .T. ) ;
#16732=ORIENTED_EDGE ( 'NONE', *, *, #43208, .F. ) ;
#16749=DIRECTION ( 'NONE',  ( 1.000000000000000000, 0.000000000000000000, 0.000000000000000000 ) ) ;
#16774=ORIENTED_EDGE ( 'NONE', *, *, #12788, .F. ) ;
#16796=VERTEX_POINT ( 'NONE', #31520 ) ;
#16810=CIRCLE ( 'NONE', #10720, 0.1574803149606299191 ) ;
#16841=CARTESIAN_POINT ( 'NONE',  ( 0.2559055118110236116, 0.1222388761248534295, -0.2994676661288905861 ) ) ;
#16844=DIRECTION ( 'NONE',  ( 0.000000000000000000, 0.000000000000000000, 1.000000000000000000 ) ) ;
#16855=EDGE_LOOP ( 'NONE', ( #22122, #18904, #35570, #41652 ) ) ;
#16859=VERTEX_POINT ( 'NONE', #8249 ) ;
#16901=CARTESIAN_POINT ( 'NONE',  ( -0.1677835123531180861, 0.1986243762397535695, -0.03618545512905874811 ) ) ;
#16914=CARTESIAN_POINT ( 'NONE',  ( 0.1574803149606299191, 1.928577636452524610E-17, -0.1574803149606298636 ) ) ;
#16954=CARTESIAN_POINT ( 'NONE',  ( -0.2559055241377596879, 0.07349206531156367295, -0.3089908134149170760 ) ) ;
#16955=FACE_OUTER_BOUND ( 'NONE', #6600, .T. ) ;
#16961=LINE ( 'NONE', #1866, #42191 ) ;
#16968=DIRECTION ( 'NONE',  ( 0.000000000000000000, 0.000000000000000000, 1.000000000000000000 ) ) ;
#16977=AXIS2_PLACEMENT_3D ( 'NONE', #38672, #15933, #30800 ) ;
#17003=CARTESIAN_POINT ( 'NONE',  ( 0.2559055118110236116, -4.594920972184172978E-16, -0.02740704184215071032 ) ) ;
#17011=ORIENTED_EDGE ( 'NONE', *, *, #16413, .F. ) ;
#17015=VECTOR ( 'NONE', #42466, 39.37007874015748854 ) ;
#17024=CARTESIAN_POINT ( 'NONE',  ( 0.01990234270466926386, -0.2840036093443640275, -0.08759220388353182452 ) ) ;
#17048=CONICAL_SURFACE ( 'NONE', #43821, 0.1377952755905510474, 0.9599310885968920237 ) ;
#17117=COLOUR_RGB ( '', 0.66274510, 0.83137255, 0.94901961) ;
#17123=CARTESIAN_POINT ( 'NONE',  ( -0.1574803149606299191, 0.000000000000000000, -0.1183602362204724257 ) ) ;
#17131=CARTESIAN_POINT ( 'NONE',  ( -0.06200172126964421937, 0.2596975217971581040, -0.05114647357131848343 ) ) ;
#17136=CARTESIAN_POINT ( 'NONE',  ( 0.1574803149606299191, 1.928577636452524610E-17, -0.04012007874015743186 ) ) ;
#17149=EDGE_CURVE ( 'NONE', #2, #45855, #17564, .T. ) ;
#17198=CIRCLE ( 'NONE', #5771, 0.1574803149606299191 ) ;
#17214=CIRCLE ( 'NONE', #42469, 0.2559055118110236116 ) ;
#17257=EDGE_CURVE ( 'NONE', #34984, #23841, #40996, .T. ) ;
#17258=CARTESIAN_POINT ( 'NONE',  ( 0.1595947434767874262, 0.2033521641548338144, -0.03294411891277416321 ) ) ;
#17321=CARTESIAN_POINT ( 'NONE',  ( 0.1738065908861024245, -0.1951474930446358835, -0.3118411609178733390 ) ) ;
#17344=CARTESIAN_POINT ( 'NONE',  ( 0.2559055118110236116, -0.1477471161312047254, -0.1122047244094488277 ) ) ;
#17365=ADVANCED_FACE ( 'NONE', ( #742 ), #33777, .F. ) ;
#17476=( NAMED_UNIT ( * ) PLANE_ANGLE_UNIT ( ) SI_UNIT ( $, .RADIAN. ) ) ;
#17487=CARTESIAN_POINT ( 'NONE',  ( 0.03889724126169821078, -0.2730368995492337691, -0.06846571731931765104 ) ) ;
#17494=CARTESIAN_POINT ( 'NONE',  ( 0.000000000000000000, 0.000000000000000000, -0.02633646578327370619 ) ) ;
#17534=CARTESIAN_POINT ( 'NONE',  ( -0.1279527559055118058, -0.2216206741968047289, -0.3149606299212598381 ) ) ;
#17539=CARTESIAN_POINT ( 'NONE',  ( 0.2559055118110236116, 0.000000000000000000, -0.3149606299212598381 ) ) ;
#17545=FACE_OUTER_BOUND ( 'NONE', #37967, .T. ) ;
#17561=CARTESIAN_POINT ( 'NONE',  ( -0.1377952755905510751, 1.687505431895958263E-17, -0.02633646578327370619 ) ) ;
#17564=LINE ( 'NONE', #31731, #29951 ) ;
#17570=CARTESIAN_POINT ( 'NONE',  ( 0.1377952755905510196, 1.687505431895957030E-17, -0.1828167807439035619 ) ) ;
#17586=CYLINDRICAL_SURFACE ( 'NONE', #37433, 0.1377952755905512694 ) ;
#17594=AXIS2_PLACEMENT_3D ( 'NONE', #7967, #4344, #19221 ) ;
#17601=CARTESIAN_POINT ( 'NONE',  ( -0.09631076833422043404, 0.2398891842387853301, -0.03294411891277443383 ) ) ;
#17625=DIMENSIONAL_EXPONENTS ( 1.000000000000000000, 0.000000000000000000, 0.000000000000000000, 0.000000000000000000, 0.000000000000000000, 0.000000000000000000, 0.000000000000000000 ) ;
#17675=DIRECTION ( 'NONE',  ( 0.000000000000000000, 0.000000000000000000, 1.000000000000000000 ) ) ;
#17685=EDGE_LOOP ( 'NONE', ( #16562, #35863, #14651, #32540 ) ) ;
#17694=VECTOR ( 'NONE', #9069, 39.37007874015748854 ) ;
#17701=CARTESIAN_POINT ( 'NONE',  ( 0.2559054503028028726, 0.07924707884460499563, -0.05308369988359751268 ) ) ;
#17713=SHAPE_REPRESENTATION_RELATIONSHIP ( 'NONE' , 'NONE' ,  #1042, #12440 ) ;
#17726=CARTESIAN_POINT ( 'NONE',  ( 0.05712600390865848338, -0.2625125185280174911, -0.05471869868084958122 ) ) ;
#17741=VERTEX_POINT ( 'NONE', #30721 ) ;
#17813=CARTESIAN_POINT ( 'NONE',  ( -0.05473415491935922084, -0.2638934531858492805, -0.05654496252297270403 ) ) ;
#17825=ORIENTED_EDGE ( 'NONE', *, *, #42405, .T. ) ;
#17833=( GEOMETRIC_REPRESENTATION_CONTEXT ( 3 ) GLOBAL_UNCERTAINTY_ASSIGNED_CONTEXT ( ( #32214 ) ) GLOBAL_UNIT_ASSIGNED_CONTEXT ( ( #35928, #17476, #2381 ) ) REPRESENTATION_CONTEXT ( 'NONE', 'WORKASPACE' ) ) ;
#17864=EDGE_CURVE ( 'NONE', #13286, #24988, #21073, .T. ) ;
#17899=CARTESIAN_POINT ( 'NONE',  ( -2.680625843783058887E-15, -0.2954942322624074524, -0.2921040715117803055 ) ) ;
#17904=PLANE ( 'NONE',  #43713 ) ;
#17912=CARTESIAN_POINT ( 'NONE',  ( 0.000000000000000000, 0.000000000000000000, -0.2219368594840610276 ) ) ;
#17918=FACE_OUTER_BOUND ( 'NONE', #44080, .T. ) ;
#17959=EDGE_CURVE ( 'NONE', #6423, #954, #3905, .T. ) ;
#17972=DIRECTION ( 'NONE',  ( 0.000000000000000000, 0.000000000000000000, 1.000000000000000000 ) ) ;
#18007=ADVANCED_FACE ( 'NONE', ( #7409 ), #20726, .F. ) ;
#18064=ORIENTED_EDGE ( 'NONE', *, *, #41719, .F. ) ;
#18138=CARTESIAN_POINT ( 'NONE',  ( 0.1089815878294855545, -0.2325720113810400280, -0.3144321013757211958 ) ) ;
#18160=DIRECTION ( 'NONE',  ( -1.000000000000000000, 0.000000000000000000, 0.000000000000000000 ) ) ;
#18197=CARTESIAN_POINT ( 'NONE',  ( 0.2559055118110236116, -4.594920972184172978E-16, -0.02740704184215071032 ) ) ;
#18203=DIRECTION ( 'NONE',  ( -0.000000000000000000, -0.000000000000000000, -1.000000000000000000 ) ) ;
#18237=CARTESIAN_POINT ( 'NONE',  ( 0.000000000000000000, 0.000000000000000000, -0.05390369169704170571 ) ) ;
#18267=CARTESIAN_POINT ( 'NONE',  ( -0.1574803149606299191, 1.928577636452524610E-17, -0.3149606299212598381 ) ) ;
#18286=CARTESIAN_POINT ( 'NONE',  ( -0.1541343738003721486, -0.2065047100573886574, -0.03112915705354596732 ) ) ;
#18307=EDGE_CURVE ( 'NONE', #40880, #19150, #31604, .T. ) ;
#18308=CARTESIAN_POINT ( 'NONE',  ( 0.2559055118110236116, 0.1477471161312027548, -0.3149606299212598381 ) ) ;
#18438=EDGE_CURVE ( 'NONE', #28768, #7920, #4676, .T. ) ;
#18445=AXIS2_PLACEMENT_3D ( 'NONE', #46950, #18203, #28785 ) ;
#18459=EDGE_CURVE ( 'NONE', #19657, #34936, #25096, .T. ) ;
#18472=CIRCLE ( 'NONE', #14650, 0.1574803149606299191 ) ;
#18482=FILL_AREA_STYLE_COLOUR ( '', #17117 ) ;
#18518=CARTESIAN_POINT ( 'NONE',  ( -0.1647197266561004347, -0.2003932537366667210, -0.03489849683095793548 ) ) ;
#18541=AXIS2_PLACEMENT_3D ( 'NONE', #33381, #14441, #29578 ) ;
#18543=PRODUCT_CONTEXT ( 'NONE', #10140, 'mechanical' ) ;
#18559=DIRECTION ( 'NONE',  ( 0.000000000000000000, 0.000000000000000000, 1.000000000000000000 ) ) ;
#18560=DIRECTION ( 'NONE',  ( 0.000000000000000000, 0.000000000000000000, 1.000000000000000000 ) ) ;
#18573=VERTEX_POINT ( 'NONE', #10975 ) ;
#18574=AXIS2_PLACEMENT_3D ( 'NONE', #13293, #27922, #2712 ) ;
#18581=CARTESIAN_POINT ( 'NONE',  ( -0.1818270763433404713, 0.1905157801856738331, -0.3106979152243534159 ) ) ;
#18590=EDGE_CURVE ( 'NONE', #23202, #43509, #21869, .T. ) ;
#18598=CARTESIAN_POINT ( 'NONE',  ( 0.1171060910386464843, -0.2278812977170392440, -0.3148284977848750943 ) ) ;
#18602=ADVANCED_FACE ( 'NONE', ( #13836 ), #17904, .T. ) ;
#18641=ORIENTED_EDGE ( 'NONE', *, *, #42405, .F. ) ;
#18642=ORIENTED_EDGE ( 'NONE', *, *, #31785, .F. ) ;
#18657=VERTEX_POINT ( 'NONE', #23156 ) ;
#18699=VERTEX_POINT ( 'NONE', #26768 ) ;
#18767=DIRECTION ( 'NONE',  ( 1.000000000000000000, 0.000000000000000000, 0.000000000000000000 ) ) ;
#18828=VECTOR ( 'NONE', #37738, 39.37007874015748143 ) ;
#18902=DIRECTION ( 'NONE',  ( 0.000000000000000000, -1.000000000000000000, 0.000000000000000000 ) ) ;
#18904=ORIENTED_EDGE ( 'NONE', *, *, #7808, .T. ) ;
#18922=AXIS2_PLACEMENT_3D ( 'NONE', #14516, #7077, #25786 ) ;
#18934=ORIENTED_EDGE ( 'NONE', *, *, #28623, .T. ) ;
#18942=PRESENTATION_STYLE_ASSIGNMENT (( #22306 ) ) ;
#18977=FACE_OUTER_BOUND ( 'NONE', #4537, .T. ) ;
#19021=CARTESIAN_POINT ( 'NONE',  ( -0.1574803149606299191, 1.928577636452524610E-17, -0.2357204724409448504 ) ) ;
#19049=CARTESIAN_POINT ( 'NONE',  ( 0.000000000000000000, 0.000000000000000000, -0.0009999999999999347518 ) ) ;
#19058=LINE ( 'NONE', #30140, #16206 ) ;
#19111=CARTESIAN_POINT ( 'NONE',  ( 0.2559055096563123688, -0.08274376297360711008, -0.05534801676208721266 ) ) ;
#19114=VECTOR ( 'NONE', #31155, 39.37007874015748143 ) ;
#19117=EDGE_LOOP ( 'NONE', ( #20577, #20567, #40641, #29246 ) ) ;
#19127=ORIENTED_EDGE ( 'NONE', *, *, #4092, .T. ) ;
#19136=EDGE_LOOP ( 'NONE', ( #22926, #9736, #27564, #21308 ) ) ;
#19150=VERTEX_POINT ( 'NONE', #39165 ) ;
#19151=ORIENTED_EDGE ( 'NONE', *, *, #29884, .T. ) ;
#19164=CIRCLE ( 'NONE', #26859, 0.1574803149606299191 ) ;
#19181=FILL_AREA_STYLE ('',( #18482 ) ) ;
#19198=FACE_OUTER_BOUND ( 'NONE', #11531, .T. ) ;
#19220=ORIENTED_EDGE ( 'NONE', *, *, #31353, .T. ) ;
#19221=DIRECTION ( 'NONE',  ( 1.000000000000000000, 0.000000000000000000, 0.000000000000000000 ) ) ;
#19222=ORIENTED_EDGE ( 'NONE', *, *, #25714, .T. ) ;
#19256=VECTOR ( 'NONE', #7982, 39.37007874015748143 ) ;
#19268=ORIENTED_EDGE ( 'NONE', *, *, #23334, .T. ) ;
#19284=DIRECTION ( 'NONE',  ( -0.000000000000000000, -0.000000000000000000, -1.000000000000000000 ) ) ;
#19300=AXIS2_PLACEMENT_3D ( 'NONE', #1862, #42350, #9545 ) ;
#19323=CARTESIAN_POINT ( 'NONE',  ( 0.2559055118110236116, -0.1477471161312049197, -0.2921040715117803055 ) ) ;
#19335=LINE ( 'NONE', #7840, #3066 ) ;
#19352=B_SPLINE_CURVE_WITH_KNOTS ( 'NONE', 3,
 ( #29218, #43766, #18598, #18138, #32782, #22432, #33017, #21738, #43522, #22677, #37278, #33490, #36370, #11202, #36829, #7816, #17899 ),
 .UNSPECIFIED., .F., .F.,
 ( 4, 2, 2, 2, 2, 1, 2, 2, 4 ),
 ( 0.000000000000000000, 0.1249999999999995004, 0.1874999999999994171, 0.2499999999999993339, 0.3749999999999992784, 0.4374999999999990563, 0.4687499999999990563, 0.4999999999999990008, 1.000000000000000000 ),
 .UNSPECIFIED. ) ;
#19378=CARTESIAN_POINT ( 'NONE',  ( 0.000000000000000000, 0.000000000000000000, -0.01478361295688420882 ) ) ;
#19400=CARTESIAN_POINT ( 'NONE',  ( -2.680625843783058887E-15, -0.2954942322624074524, -0.2921040715117803055 ) ) ;
#19472=EDGE_LOOP ( 'NONE', ( #45614, #32323, #19803, #37094 ) ) ;
#19475=ADVANCED_FACE ( 'NONE', ( #26713 ), #27440, .F. ) ;
#19481=ORIENTED_EDGE ( 'NONE', *, *, #34878, .T. ) ;
#19482=EDGE_CURVE ( 'NONE', #20308, #40149, #37717, .T. ) ;
#19492=DIRECTION ( 'NONE',  ( 0.000000000000000000, 0.000000000000000000, 1.000000000000000000 ) ) ;
#19495=VECTOR ( 'NONE', #15796, 39.37007874015748143 ) ;
#19500=CARTESIAN_POINT ( 'NONE',  ( -0.1574803149606299191, 1.928577636452524610E-17, 2.731847993664263218E-16 ) ) ;
#19516=CARTESIAN_POINT ( 'NONE',  ( -0.1377952755905510751, 1.687505431895957647E-17, -0.3149606299212598381 ) ) ;
#19555=CARTESIAN_POINT ( 'NONE',  ( -0.1469224761500225462, -0.2106668292959394673, -0.3144321013757213623 ) ) ;
#19598=ORIENTED_EDGE ( 'NONE', *, *, #39152, .F. ) ;
#19657=VERTEX_POINT ( 'NONE', #32191 ) ;
#19675=DIRECTION ( 'NONE',  ( -1.000000000000000000, 0.000000000000000000, 0.000000000000000000 ) ) ;
#19691=DIRECTION ( 'NONE',  ( -0.8660254037844382635, 0.5000000000000007772, 0.000000000000000000 ) ) ;
#19698=CARTESIAN_POINT ( 'NONE',  ( -0.2559055118110236671, -0.08239886119520901941, -0.05512121553257845474 ) ) ;
#19733=CARTESIAN_POINT ( 'NONE',  ( 0.2449982982384770469, -0.1540443988234191652, -0.2957398093692971686 ) ) ;
#19759=EDGE_LOOP ( 'NONE', ( #7430, #16111, #35285, #2424 ) ) ;
#19761=ADVANCED_FACE ( 'NONE', ( #30219 ), #35261, .T. ) ;
#19771=ORIENTED_EDGE ( 'NONE', *, *, #7379, .F. ) ;
#19803=ORIENTED_EDGE ( 'NONE', *, *, #15366, .F. ) ;
#19807=ADVANCED_FACE ( 'NONE', ( #44528, #1161 ), #33802, .F. ) ;
#19820=CARTESIAN_POINT ( 'NONE',  ( -0.1977610074736072532, 0.1813162243850413025, -0.3078067560680682324 ) ) ;
#19851=DIRECTION ( 'NONE',  ( 1.000000000000000000, 0.000000000000000000, 0.000000000000000000 ) ) ;
#19877=CARTESIAN_POINT ( 'NONE',  ( 0.09011016336849961283, 0.2434714151302298513, -0.3128311589625373812 ) ) ;
#19904=CARTESIAN_POINT ( 'NONE',  ( 0.1964094517284671326, 0.1820971824355889779, -0.05295753290289392790 ) ) ;
#19926=ORIENTED_EDGE ( 'NONE', *, *, #2957, .F. ) ;
#19932=VECTOR ( 'NONE', #16118, 39.37007874015748854 ) ;
#19959=DIRECTION ( 'NONE',  ( 1.000000000000000000, 0.000000000000000000, 0.000000000000000000 ) ) ;
#20024=CARTESIAN_POINT ( 'NONE',  ( -0.1550611416717992963, -0.2059691479693902261, -0.3138705397960867005 ) ) ;
#20046=CARTESIAN_POINT ( 'NONE',  ( 0.1377952755905513804, 1.687505431895961653E-17, -0.3001770169643759867 ) ) ;
#20054=CARTESIAN_POINT ( 'NONE',  ( -0.2343326035689475839, 0.1601959449158263660, -0.2989494884452092993 ) ) ;
#20075=CYLINDRICAL_SURFACE ( 'NONE', #43920, 0.1377952755905511306 ) ;
#20099=DIRECTION ( 'NONE',  ( 1.000000000000000000, 0.000000000000000000, 0.000000000000000000 ) ) ;
#20167=CARTESIAN_POINT ( 'NONE',  ( -0.1377952755905509363, 1.687505431895957030E-17, -0.1045766232635885612 ) ) ;
#20177=EDGE_LOOP ( 'NONE', ( #30591, #47424, #1478, #4063 ) ) ;
#20202=FACE_OUTER_BOUND ( 'NONE', #41434, .T. ) ;
#20226=FACE_OUTER_BOUND ( 'NONE', #32748, .T. ) ;
#20249=AXIS2_PLACEMENT_3D ( 'NONE', #31303, #39161, #2733 ) ;
#20254=CARTESIAN_POINT ( 'NONE',  ( -0.1997612633124555837, 0.1801620131153011950, -0.05546260682012547211 ) ) ;
#20277=CIRCLE ( 'NONE', #15039, 0.1377952755905509363 ) ;
#20284=AXIS2_PLACEMENT_3D ( 'NONE', #42427, #42194, #31690 ) ;
#20307=CARTESIAN_POINT ( 'NONE',  ( 0.000000000000000000, 0.000000000000000000, -0.3149606299212598381 ) ) ;
#20308=VERTEX_POINT ( 'NONE', #42531 ) ;
#20331=DIRECTION ( 'NONE',  ( -0.000000000000000000, -0.000000000000000000, -1.000000000000000000 ) ) ;
#20335=ORIENTED_EDGE ( 'NONE', *, *, #42444, .F. ) ;
#20362=CIRCLE ( 'NONE', #3530, 0.1567662409572586624 ) ;
#20398=CARTESIAN_POINT ( 'NONE',  ( 0.000000000000000000, 0.000000000000000000, 2.731847993664263218E-16 ) ) ;
#20400=CARTESIAN_POINT ( 'NONE',  ( 0.1377952755905510751, 0.000000000000000000, -0.3149606299212598381 ) ) ;
#20423=CARTESIAN_POINT ( 'NONE',  ( 0.1377952755905511306, 0.000000000000000000, -0.3149606299212598381 ) ) ;
#20442=DIRECTION ( 'NONE',  ( 1.000000000000000000, 0.000000000000000000, 0.000000000000000000 ) ) ;
#20466=ORIENTED_EDGE ( 'NONE', *, *, #21253, .F. ) ;
#20469=CARTESIAN_POINT ( 'NONE',  ( 0.1994795808946360216, -0.1803246425350570614, -0.05524818609633110750 ) ) ;
#20472=VECTOR ( 'NONE', #44422, 39.37007874015748143 ) ;
#20473=DIRECTION ( 'NONE',  ( 0.8191520442889873577, 0.000000000000000000, 0.5735764363510523767 ) ) ;
#20480=ORIENTED_EDGE ( 'NONE', *, *, #45312, .F. ) ;
#20489=CONICAL_SURFACE ( 'NONE', #562, 0.1574803149606299191, 0.9599310885968713736 ) ;
#20491=CARTESIAN_POINT ( 'NONE',  ( -0.1849324350982172738, 0.1887234410765585568, -0.04495255068435553836 ) ) ;
#20535=LINE ( 'NONE', #45447, #9597 ) ;
#20561=CARTESIAN_POINT ( 'NONE',  ( 0.000000000000000000, 0.000000000000000000, -0.3001770169643759867 ) ) ;
#20567=ORIENTED_EDGE ( 'NONE', *, *, #44394, .F. ) ;
#20577=ORIENTED_EDGE ( 'NONE', *, *, #9039, .F. ) ;
#20593=AXIS2_PLACEMENT_3D ( 'NONE', #39346, #45831, #20442 ) ;
#20603=CYLINDRICAL_SURFACE ( 'NONE', #14829, 0.1377952755905510751 ) ;
#20606=AXIS2_PLACEMENT_3D ( 'NONE', #24242, #10088, #38605 ) ;
#20609=CARTESIAN_POINT ( 'NONE',  ( 0.1677835123531307704, -0.1986243762397479629, -0.03618545512907316714 ) ) ;
#20631=CIRCLE ( 'NONE', #32914, 0.1574803149606299191 ) ;
#20678=DIRECTION ( 'NONE',  ( 1.000000000000000000, 0.000000000000000000, 0.000000000000000000 ) ) ;
#20726=CONICAL_SURFACE ( 'NONE', #18445, 0.1377952755905509363, 0.9599310885968936891 ) ;
#20776=ORIENTED_EDGE ( 'NONE', *, *, #35537, .F. ) ;
#20814=CARTESIAN_POINT ( 'NONE',  ( 0.06197108496688099460, 0.2597152231171855341, -0.3085539532670620311 ) ) ;
#20832=EDGE_CURVE ( 'NONE', #26918, #873, #46387, .T. ) ;
#20836=LENGTH_MEASURE_WITH_UNIT ( LENGTH_MEASURE( 0.02539999999999999897 ), #39735 ) ;
#20843=CARTESIAN_POINT ( 'NONE',  ( 0.1404189863467218691, -0.2144232926957947427, -0.02742975588281126517 ) ) ;
#20845=CARTESIAN_POINT ( 'NONE',  ( 0.08985779549332124916, 0.2436148098455510058, -0.03544556188504843774 ) ) ;
#20860=AXIS2_PLACEMENT_3D ( 'NONE', #25692, #32652, #10835 ) ;
#20861=CONICAL_SURFACE ( 'NONE', #2495, 0.1567662409572586624, 0.9599310885969887241 ) ;
#20865=CARTESIAN_POINT ( 'NONE',  ( 0.000000000000000000, 0.000000000000000000, -0.3149606299212598381 ) ) ;
#20871=AXIS2_PLACEMENT_3D ( 'NONE', #34733, #4098, #19851 ) ;
#20974=ORIENTED_EDGE ( 'NONE', *, *, #21276, .F. ) ;
#21022=DIRECTION ( 'NONE',  ( 1.000000000000000000, 0.000000000000000000, 0.000000000000000000 ) ) ;
#21025=AXIS2_PLACEMENT_3D ( 'NONE', #29955, #12671, #22961 ) ;
#21068=CARTESIAN_POINT ( 'NONE',  ( 0.000000000000000000, 0.000000000000000000, -0.3149606299212598381 ) ) ;
#21073=LINE ( 'NONE', #32372, #23832 ) ;
#21075=CARTESIAN_POINT ( 'NONE',  ( 0.09357655176633394856, -0.2414677849102791207, -0.03395687952546033034 ) ) ;
#21097=EDGE_CURVE ( 'NONE', #18573, #40024, #4675, .T. ) ;
#21110=DIRECTION ( 'NONE',  ( -0.8191520442889991260, 0.000000000000000000, -0.5735764363510355013 ) ) ;
#21119=EDGE_CURVE ( 'NONE', #28934, #18699, #10838, .T. ) ;
#21141=CARTESIAN_POINT ( 'NONE',  ( 0.1711365707900877331, -0.1966896243418751189, -0.3121915932859509191 ) ) ;
#21186=CARTESIAN_POINT ( 'NONE',  ( -0.2151545284320415252, 0.1712747073548011034, -0.06815351164859909106 ) ) ;
#21232=DIRECTION ( 'NONE',  ( 1.000000000000000000, 0.000000000000000000, 0.000000000000000000 ) ) ;
#21237=CARTESIAN_POINT ( 'NONE',  ( 0.000000000000000000, 0.000000000000000000, -0.3149606299212598381 ) ) ;
#21241=ORIENTED_EDGE ( 'NONE', *, *, #43050, .F. ) ;
#21253=EDGE_CURVE ( 'NONE', #8606, #15186, #24248, .T. ) ;
#21257=CARTESIAN_POINT ( 'NONE',  ( -0.2559055118110236116, -4.908314874579054539E-16, -0.02740704184215039460 ) ) ;
#21275=CYLINDRICAL_SURFACE ( 'NONE', #46680, 0.1377952755905510751 ) ;
#21276=EDGE_CURVE ( 'NONE', #21602, #7313, #46793, .T. ) ;
#21289=CARTESIAN_POINT ( 'NONE',  ( 0.2559043235492289292, 0.06578104287837578668, -0.04518399471589295419 ) ) ;
#21308=ORIENTED_EDGE ( 'NONE', *, *, #3018, .F. ) ;
#21309=CARTESIAN_POINT ( 'NONE',  ( 0.000000000000000000, 0.000000000000000000, -0.1828167807439035619 ) ) ;
#21359=DIRECTION ( 'NONE',  ( 0.000000000000000000, 0.000000000000000000, 1.000000000000000000 ) ) ;
#21360=FACE_OUTER_BOUND ( 'NONE', #28584, .T. ) ;
#21366=CARTESIAN_POINT ( 'NONE',  ( 0.2559055118110236116, -0.09499862663905693505, -0.3051626384476439635 ) ) ;
#21374=DIRECTION ( 'NONE',  ( 1.000000000000000000, 0.000000000000000000, 0.000000000000000000 ) ) ;
#21390=EDGE_LOOP ( 'NONE', ( #26714, #7714, #43990, #24094 ) ) ;
#21413=ORIENTED_EDGE ( 'NONE', *, *, #31931, .F. ) ;
#21451=EDGE_LOOP ( 'NONE', ( #28328, #26340, #16246, #16732 ) ) ;
#21456=ORIENTED_EDGE ( 'NONE', *, *, #31785, .T. ) ;
#21493=CARTESIAN_POINT ( 'NONE',  ( -0.2559055118110236671, 0.04128066261331859998, -0.03449252736539444586 ) ) ;
#21502=EDGE_LOOP ( 'NONE', ( #19598, #13471, #21788, #1351 ) ) ;
#21518=AXIS2_PLACEMENT_3D ( 'NONE', #15973, #37517, #30596 ) ;
#21528=CARTESIAN_POINT ( 'NONE',  ( 0.2559055118110210025, 0.007196880244715129354, -0.02740704184215201136 ) ) ;
#21572=ORIENTED_EDGE ( 'NONE', *, *, #32539, .T. ) ;
#21573=ORIENTED_EDGE ( 'NONE', *, *, #16669, .F. ) ;
#21593=ADVANCED_FACE ( 'NONE', ( #36605 ), #5515, .T. ) ;
#21598=ORIENTED_EDGE ( 'NONE', *, *, #33900, .F. ) ;
#21602=VERTEX_POINT ( 'NONE', #39695 ) ;
#21617=CIRCLE ( 'NONE', #5535, 0.1574803149606299191 ) ;
#21626=AXIS2_PLACEMENT_3D ( 'NONE', #16566, #26892, #19675 ) ;
#21642=ORIENTED_EDGE ( 'NONE', *, *, #32450, .F. ) ;
#21648=CARTESIAN_POINT ( 'NONE',  ( -0.1987795079023651490, -0.1807288298655959913, -0.05471869868084799915 ) ) ;
#21706=EDGE_CURVE ( 'NONE', #13443, #752, #39940, .T. ) ;
#21738=CARTESIAN_POINT ( 'NONE',  ( 0.09005431033085642412, -0.2435012976189759315, -0.3128573757127792176 ) ) ;
#21745=DIRECTION ( 'NONE',  ( 0.000000000000000000, 0.000000000000000000, 1.000000000000000000 ) ) ;
#21785=VERTEX_POINT ( 'NONE', #11684 ) ;
#21788=ORIENTED_EDGE ( 'NONE', *, *, #43210, .T. ) ;
#21809=VERTEX_POINT ( 'NONE', #16914 ) ;
#21835=VECTOR ( 'NONE', #10050, 39.37007874015748143 ) ;
#21869=B_SPLINE_CURVE_WITH_KNOTS ( 'NONE', 3,
 ( #21257, #3755, #13596, #28234, #32313, #39686, #21493, #42797, #32787, #24626, #47382, #47142, #32064, #39463, #29224, #36125, #43771, #39933, #14326, #25591, #46652 ),
 .UNSPECIFIED., .F., .F.,
 ( 4, 1, 1, 1, 1, 2, 2, 1, 1, 1, 1, 1, 2, 2, 4 ),
 ( 0.000000000000000000, 0.1249999999999975298, 0.1874999999999962808, 0.2187499999999956701, 0.2343749999999953926, 0.2421874999999951983, 0.2499999999999949762, 0.3749999999999932832, 0.4374999999999924505, 0.4687499999999920064, 0.4843749999999918954, 0.4921874999999918399, 0.4960937499999916733, 0.4999999999999915623, 1.000000000000000000 ),
 .UNSPECIFIED. ) ;
#21886=DIRECTION ( 'NONE',  ( -0.000000000000000000, -0.000000000000000000, -1.000000000000000000 ) ) ;
#21887=CARTESIAN_POINT ( 'NONE',  ( -0.1432458882847533199, -0.2127911801008985637, -0.02834147079957508031 ) ) ;
#21953=CARTESIAN_POINT ( 'NONE',  ( -0.1495543973312470909, 0.2091518620004931273, -0.3144333452974443222 ) ) ;
#21983=CARTESIAN_POINT ( 'NONE',  ( 0.000000000000000000, 0.000000000000000000, -0.3149606299212598381 ) ) ;
#22046=ORIENTED_EDGE ( 'NONE', *, *, #28433, .F. ) ;
#22064=DIRECTION ( 'NONE',  ( 1.000000000000000000, 0.000000000000000000, 0.000000000000000000 ) ) ;
#22098=VERTEX_POINT ( 'NONE', #15701 ) ;
#22105=CARTESIAN_POINT ( 'NONE',  ( -0.1154865254642846034, -0.2288180556978286484, -0.02742975588280020111 ) ) ;
#22122=ORIENTED_EDGE ( 'NONE', *, *, #23171, .F. ) ;
#22128=PLANE ( 'NONE',  #23303 ) ;
#22135=AXIS2_PLACEMENT_3D ( 'NONE', #7144, #2355, #6895 ) ;
#22169=CARTESIAN_POINT ( 'NONE',  ( -0.2559055118110236116, -0.1477471161312049197, -0.1122047244094488277 ) ) ;
#22172=EDGE_CURVE ( 'NONE', #17741, #19150, #31535, .T. ) ;
#22190=ADVANCED_FACE ( 'NONE', ( #42245 ), #41435, .F. ) ;
#22306=SURFACE_STYLE_USAGE ( .BOTH. , #26164 ) ;
#22375=CARTESIAN_POINT ( 'NONE',  ( -0.03889724126169491480, 0.2730368995492339357, -0.06846571731931054561 ) ) ;
#22386=LINE ( 'NONE', #19021, #4659 ) ;
#22402=AXIS2_PLACEMENT_3D ( 'NONE', #5547, #46023, #13235 ) ;
#22432=CARTESIAN_POINT ( 'NONE',  ( 0.1008439437011256906, -0.2372714618124188435, -0.3138705397960864785 ) ) ;
#22476=CARTESIAN_POINT ( 'NONE',  ( 0.2559054921376553993, -0.04463177124945857249, -0.03568053490012755569 ) ) ;
#22513=UNCERTAINTY_MEASURE_WITH_UNIT (LENGTH_MEASURE( 1.000000000000000082E-05 ), #7227, 'distance_accuracy_value', 'NONE') ;
#22515=ORIENTED_EDGE ( 'NONE', *, *, #4092, .F. ) ;
#22649=CARTESIAN_POINT ( 'NONE',  ( 0.000000000000000000, 0.000000000000000000, -0.1828167807439035619 ) ) ;
#22677=CARTESIAN_POINT ( 'NONE',  ( 0.07669050334470198238, -0.2512157378938873475, -0.3110703821947682357 ) ) ;
#22707=DIRECTION ( 'NONE',  ( 0.000000000000000000, 0.000000000000000000, 1.000000000000000000 ) ) ;
#22759=CARTESIAN_POINT ( 'NONE',  ( -0.09011016336854826836, -0.2434714151301908824, -0.3128311589625485389 ) ) ;
#22773=CARTESIAN_POINT ( 'NONE',  ( -0.2559098255137246536, 0.02501923667458835418, -0.3142646454376785137 ) ) ;
#22892=ORIENTED_EDGE ( 'NONE', *, *, #19482, .F. ) ;
#22926=ORIENTED_EDGE ( 'NONE', *, *, #33834, .F. ) ;
#22940=CARTESIAN_POINT ( 'NONE',  ( 0.1574803149606299191, 1.928577636452524610E-17, -0.2748405511811023438 ) ) ;
#22947=ADVANCED_FACE ( 'NONE', ( #34724 ), #12445, .F. ) ;
#22956=EDGE_CURVE ( 'NONE', #7313, #42075, #23500, .T. ) ;
#22961=DIRECTION ( 'NONE',  ( -1.000000000000000000, 0.000000000000000000, 0.000000000000000000 ) ) ;
#22981=DIRECTION ( 'NONE',  ( -0.8191520442889989040, 0.000000000000000000, -0.5735764363510359454 ) ) ;
#23001=CARTESIAN_POINT ( 'NONE',  ( -0.1279527559055118058, -0.2216206741968047289, -0.3149606299212598381 ) ) ;
#23025=CONICAL_SURFACE ( 'NONE', #36820, 0.1377952755905509363, 0.9599310885968960205 ) ;
#23047=DIRECTION ( 'NONE',  ( 1.000000000000000000, 0.000000000000000000, 0.000000000000000000 ) ) ;
#23060=CARTESIAN_POINT ( 'NONE',  ( -0.2559055118110236116, -0.1477471161312043368, -0.3149606299212598381 ) ) ;
#23066=CARTESIAN_POINT ( 'NONE',  ( -0.2559055118110236671, -0.08665008082093515751, -0.05796767012934854468 ) ) ;
#23071=CYLINDRICAL_SURFACE ( 'NONE', #7998, 0.1377952755905510751 ) ;
#23097=B_SPLINE_CURVE_WITH_KNOTS ( 'NONE', 3,
 ( #37960, #19733, #34367, #1508, #2694, #24059, #6527, #38888, #10384, #6290, #10142, #5834, #17321, #21141, #46542, #27908, #31958, #24751, #42239 ),
 .UNSPECIFIED., .F., .F.,
 ( 4, 2, 2, 1, 2, 2, 2, 2, 2, 4 ),
 ( 0.000000000000000000, 0.2500000000000028311, 0.3750000000000042188, 0.4375000000000049960, 0.4687500000000051625, 0.5000000000000052180, 0.6250000000000036637, 0.6875000000000028866, 0.7500000000000021094, 1.000000000000000000 ),
 .UNSPECIFIED. ) ;
#23101=EDGE_CURVE ( 'NONE', #38861, #23202, #2451, .T. ) ;
#23103=CARTESIAN_POINT ( 'NONE',  ( 0.000000000000000000, 0.000000000000000000, -0.1966003937007873570 ) ) ;
#23118=ORIENTED_EDGE ( 'NONE', *, *, #2269, .F. ) ;
#23124=DIRECTION ( 'NONE',  ( -1.000000000000000000, 0.000000000000000000, 0.000000000000000000 ) ) ;
#23133=ORIENTED_EDGE ( 'NONE', *, *, #5244, .T. ) ;
#23156=CARTESIAN_POINT ( 'NONE',  ( -0.1377952755905511861, 1.808041534174241898E-17, -0.01478361295688420882 ) ) ;
#23164=CARTESIAN_POINT ( 'NONE',  ( 0.1377952755905510751, 0.000000000000000000, -0.02633646578327370619 ) ) ;
#23171=EDGE_CURVE ( 'NONE', #3412, #41311, #39194, .T. ) ;
#23202=VERTEX_POINT ( 'NONE', #36490 ) ;
#23203=CARTESIAN_POINT ( 'NONE',  ( 0.000000000000000000, 0.000000000000000000, -0.09302377043719921301 ) ) ;
#23233=DIRECTION ( 'NONE',  ( 0.000000000000000000, 0.000000000000000000, 1.000000000000000000 ) ) ;
#23237=VERTEX_POINT ( 'NONE', #4321 ) ;
#23275=EDGE_CURVE ( 'NONE', #16796, #18657, #3994, .T. ) ;
#23285=DIRECTION ( 'NONE',  ( 0.000000000000000000, 0.000000000000000000, 1.000000000000000000 ) ) ;
#23303=AXIS2_PLACEMENT_3D ( 'NONE', #18308, #7981, #29622 ) ;
#23307=CARTESIAN_POINT ( 'NONE',  ( -0.2559055118110236116, -0.1194803229784886650, -0.08356133691647003869 ) ) ;
#23326=DIRECTION ( 'NONE',  ( 0.000000000000000000, 0.000000000000000000, 1.000000000000000000 ) ) ;
#23334=EDGE_CURVE ( 'NONE', #370, #17741, #23694, .T. ) ;
#23341=CARTESIAN_POINT ( 'NONE',  ( 0.000000000000000000, 0.000000000000000000, -0.1183602362204724257 ) ) ;
#23344=AXIS2_PLACEMENT_3D ( 'NONE', #23203, #8333, #5451 ) ;
#23357=ORIENTED_EDGE ( 'NONE', *, *, #10741, .T. ) ;
#23367=CARTESIAN_POINT ( 'NONE',  ( 0.1333875707378843478, 0.2184828823903391670, -0.3149606299212599492 ) ) ;
#23401=AXIS2_PLACEMENT_3D ( 'NONE', #36144, #18160, #25605 ) ;
#23430=CARTESIAN_POINT ( 'NONE',  ( -0.2185580477446626979, 0.1693028889594568043, -0.3031249188861500632 ) ) ;
#23449=CARTESIAN_POINT ( 'NONE',  ( -0.2559055118110236116, 0.1477471161312047254, -0.2921040715117803055 ) ) ;
#23454=CARTESIAN_POINT ( 'NONE',  ( 0.000000000000000000, 0.000000000000000000, -0.3149606299212598381 ) ) ;
#23474=CARTESIAN_POINT ( 'NONE',  ( 3.414809992080330995E-16, 0.2954942322624074524, 0.000000000000000000 ) ) ;
#23500=B_SPLINE_CURVE_WITH_KNOTS ( 'NONE', 3,
 ( #28611, #2689, #39341, #3163, #25219, #27903, #6283, #2221, #39810, #28849, #16841, #38881 ),
 .UNSPECIFIED., .F., .F.,
 ( 4, 1, 1, 1, 1, 2, 2, 4 ),
 ( 0.000000000000000000, 0.2500000000000017208, 0.3750000000000024425, 0.4375000000000028311, 0.4687500000000029976, 0.4843750000000031641, 0.5000000000000033307, 1.000000000000000000 ),
 .UNSPECIFIED. ) ;
#23507=ADVANCED_FACE ( 'NONE', ( #5225 ), #37700, .F. ) ;
#23508=ORIENTED_EDGE ( 'NONE', *, *, #43324, .T. ) ;
#23547=CARTESIAN_POINT ( 'NONE',  ( -0.2559055118110235560, -0.08435794557227528634, -0.05641901976107029787 ) ) ;
#23597=AXIS2_PLACEMENT_3D ( 'NONE', #8972, #37737, #34624 ) ;
#23615=CARTESIAN_POINT ( 'NONE',  ( -0.2559061271197219378, -0.05275274989394477393, -0.3118637899121943780 ) ) ;
#23634=PLANE ( 'NONE',  #45964 ) ;
#23645=ORIENTED_EDGE ( 'NONE', *, *, #30937, .F. ) ;
#23667=AXIS2_PLACEMENT_3D ( 'NONE', #14568, #7377, #44473 ) ;
#23674=DIRECTION ( 'NONE',  ( 0.000000000000000000, 0.000000000000000000, 1.000000000000000000 ) ) ;
#23677=CARTESIAN_POINT ( 'NONE',  ( -0.1567662409572586624, 0.000000000000000000, -0.0004999999999998990712 ) ) ;
#23693=CARTESIAN_POINT ( 'NONE',  ( -0.1377952755905510196, 0.000000000000000000, -0.1828167807439035619 ) ) ;
#23694=LINE ( 'NONE', #8835, #4026 ) ;
#23695=LINE ( 'NONE', #34256, #11682 ) ;
#23735=ORIENTED_EDGE ( 'NONE', *, *, #11179, .T. ) ;
#23746=VECTOR ( 'NONE', #30554, 39.37007874015748143 ) ;
#23753=ADVANCED_FACE ( 'NONE', ( #20202 ), #20861, .F. ) ;
#23811=ADVANCED_FACE ( 'NONE', ( #4565 ), #32395, .F. ) ;
#23832=VECTOR ( 'NONE', #39744, 39.37007874015748143 ) ;
#23841=VERTEX_POINT ( 'NONE', #11802 ) ;
#23845=EDGE_LOOP ( 'NONE', ( #3761, #14652, #2395, #32393, #20974, #14286 ) ) ;
#23849=CARTESIAN_POINT ( 'NONE',  ( -0.2559005158470596397, -0.09846603769604915513, -0.3044373381439980930 ) ) ;
#23902=DIRECTION ( 'NONE',  ( 0.000000000000000000, 0.000000000000000000, 1.000000000000000000 ) ) ;
#23944=AXIS2_PLACEMENT_3D ( 'NONE', #2670, #28339, #6741 ) ;
#23948=ADVANCED_FACE ( 'NONE', ( #30273 ), #38361, .F. ) ;
#23978=CIRCLE ( 'NONE', #23944, 0.1377952755905513804 ) ;
#23990=ADVANCED_FACE ( 'NONE', ( #33859 ), #42279, .F. ) ;
#23994=CARTESIAN_POINT ( 'NONE',  ( 0.09016091299416212346, 0.2434398048748445675, -0.03531881253560968659 ) ) ;
#24012=DIRECTION ( 'NONE',  ( -0.8191520442889873577, 1.003171929053519323E-16, 0.5735764363510523767 ) ) ;
#24021=CARTESIAN_POINT ( 'NONE',  ( 0.1377952755905511861, 0.000000000000000000, -0.1321438491773566926 ) ) ;
#24025=ORIENTED_EDGE ( 'NONE', *, *, #45544, .T. ) ;
#24033=CARTESIAN_POINT ( 'NONE',  ( -0.09005431032995797613, 0.2435012976196485601, -0.3128573757126095756 ) ) ;
#24035=EDGE_CURVE ( 'NONE', #15682, #13443, #953, .T. ) ;
#24054=CARTESIAN_POINT ( 'NONE',  ( 0.1574803149606299191, 0.000000000000000000, -0.3149606299212598381 ) ) ;
#24059=CARTESIAN_POINT ( 'NONE',  ( 0.2055371055873737307, -0.1768241869785752152, -0.3061783854716485509 ) ) ;
#24069=ORIENTED_EDGE ( 'NONE', *, *, #4187, .F. ) ;
#24078=CARTESIAN_POINT ( 'NONE',  ( -2.458663194297838277E-15, -0.2954942322624074524, -0.1122047244094488277 ) ) ;
#24087=CARTESIAN_POINT ( 'NONE',  ( -0.1377952755905509363, 1.687505431895957030E-17, -0.1436967020037460685 ) ) ;
#24094=ORIENTED_EDGE ( 'NONE', *, *, #34878, .F. ) ;
#24095=CARTESIAN_POINT ( 'NONE',  ( -0.2559049524053137459, -0.08043145352417861715, -0.3078373565276721902 ) ) ;
#24099=VECTOR ( 'NONE', #29536, 39.37007874015748143 ) ;
#24107=CYLINDRICAL_SURFACE ( 'NONE', #20249, 0.1377952755905511306 ) ;
#24127=DIRECTION ( 'NONE',  ( 0.000000000000000000, 0.000000000000000000, 1.000000000000000000 ) ) ;
#24133=EDGE_CURVE ( 'NONE', #30017, #26580, #9379, .T. ) ;
#24168=LINE ( 'NONE', #7516, #8640 ) ;
#24230=CARTESIAN_POINT ( 'NONE',  ( 0.1647197266561027384, 0.2003932537366638067, -0.03489849683095651994 ) ) ;
#24242=CARTESIAN_POINT ( 'NONE',  ( 0.000000000000000000, 0.000000000000000000, -0.04012007874015743186 ) ) ;
#24248=LINE ( 'NONE', #42189, #32297 ) ;
#24256=EDGE_LOOP ( 'NONE', ( #29832, #6914, #14310, #29426, #39536 ) ) ;
#24291=CYLINDRICAL_SURFACE ( 'NONE', #16030, 0.1377952755905512694 ) ;
#24312=ADVANCED_FACE ( 'NONE', ( #415 ), #13261, .F. ) ;
#24315=ADVANCED_FACE ( 'NONE', ( #11459 ), #30152, .F. ) ;
#24317=LINE ( 'NONE', #38915, #46719 ) ;
#24324=CARTESIAN_POINT ( 'NONE',  ( -0.2559054651920882328, -0.06820678008027236672, -0.3098418326308006177 ) ) ;
#24334=CARTESIAN_POINT ( 'NONE',  ( -0.1126596235262965900, 0.2304501682926980155, -0.02834147079956141763 ) ) ;
#24376=DIRECTION ( 'NONE',  ( 1.000000000000000000, 0.000000000000000000, 0.000000000000000000 ) ) ;
#24399=DIRECTION ( 'NONE',  ( -0.000000000000000000, -0.000000000000000000, -1.000000000000000000 ) ) ;
#24404=VERTEX_POINT ( 'NONE', #44729 ) ;
#24450=CARTESIAN_POINT ( 'NONE',  ( 0.1706040688522296178, 0.1969959271857260608, -0.03730110279444987659 ) ) ;
#24479=CARTESIAN_POINT ( 'NONE',  ( 0.000000000000000000, 0.000000000000000000, -0.1183602362204724257 ) ) ;
#24558=CARTESIAN_POINT ( 'NONE',  ( -0.05770278849818247929, 0.2621795117899895500, -0.05428606100831778053 ) ) ;
#24618=DIRECTION ( 'NONE',  ( 0.000000000000000000, 0.000000000000000000, 1.000000000000000000 ) ) ;
#24626=CARTESIAN_POINT ( 'NONE',  ( -0.2559055118110235560, 0.04947374976879801572, -0.03739270108708937779 ) ) ;
#24654=ORIENTED_EDGE ( 'NONE', *, *, #21706, .T. ) ;
#24665=CARTESIAN_POINT ( 'NONE',  ( 0.2559054646112969289, 0.04956735787872018628, -0.03742695103908252191 ) ) ;
#24717=LINE ( 'NONE', #2659, #27918 ) ;
#24734=CARTESIAN_POINT ( 'NONE',  ( 0.1574803149606299191, 0.000000000000000000, -0.1183602362204724257 ) ) ;
#24751=CARTESIAN_POINT ( 'NONE',  ( 0.1387951811623661658, -0.2153607970560919849, -0.3149606299212599492 ) ) ;
#24774=CARTESIAN_POINT ( 'NONE',  ( 0.2011713568916692896, -0.1793478952077613708, -0.05654496252297557674 ) ) ;
#24794=PRODUCT_DEFINITION ( 'UNKNOWN', '', #14795, #43194 ) ;
#24797=CARTESIAN_POINT ( 'NONE',  ( -0.1993772601175057280, 0.1803837174632751672, -0.05517042925146035948 ) ) ;
#24836=PLANE ( 'NONE',  #15763 ) ;
#24846=FACE_OUTER_BOUND ( 'NONE', #30023, .T. ) ;
#24874=B_SPLINE_CURVE_WITH_KNOTS ( 'NONE', 3,
 ( #9234, #27939, #9713, #30837, #23849, #31530, #42507, #24095, #5876, #46112, #24324, #45872, #23615, #38922, #30594, #38226, #12376, #38463, #16664 ),
 .UNSPECIFIED., .F., .F.,
 ( 4, 2, 2, 1, 2, 2, 2, 2, 2, 4 ),
 ( 0.000000000000000000, 0.2499999999999995559, 0.3749999999999995559, 0.4374999999999996669, 0.4687499999999996669, 0.4999999999999996669, 0.6249999999999996669, 0.6874999999999997780, 0.7499999999999998890, 1.000000000000000000 ),
 .UNSPECIFIED. ) ;
#24876=AXIS2_PLACEMENT_3D ( 'NONE', #20307, #45937, #6151 ) ;
#24877=DIRECTION ( 'NONE',  ( 0.000000000000000000, 0.000000000000000000, 1.000000000000000000 ) ) ;
#24945=VECTOR ( 'NONE', #28402, 39.37007874015748143 ) ;
#24951=ADVANCED_FACE ( 'NONE', ( #13651 ), #20603, .F. ) ;
#24988=VERTEX_POINT ( 'NONE', #2617 ) ;
#25004=DIRECTION ( 'NONE',  ( -1.000000000000000000, 0.000000000000000000, 0.000000000000000000 ) ) ;
#25063=ORIENTED_EDGE ( 'NONE', *, *, #21097, .T. ) ;
#25096=LINE ( 'NONE', #28971, #38388 ) ;
#25109=DIRECTION ( 'NONE',  ( 1.000000000000000000, 0.000000000000000000, 0.000000000000000000 ) ) ;
#25178=VERTEX_POINT ( 'NONE', #18197 ) ;
#25184=DIRECTION ( 'NONE',  ( -1.000000000000000000, 1.776356839400250070E-15, 0.000000000000000000 ) ) ;
#25219=CARTESIAN_POINT ( 'NONE',  ( 0.2559055118110235560, 0.06384451362999800372, -0.3104478705636015134 ) ) ;
#25344=DIRECTION ( 'NONE',  ( 1.000000000000000000, 0.000000000000000000, 0.000000000000000000 ) ) ;
#25352=ADVANCED_FACE ( 'NONE', ( #31128 ), #20075, .F. ) ;
#25365=PLANE ( 'NONE',  #23401 ) ;
#25418=ORIENTED_EDGE ( 'NONE', *, *, #26869, .F. ) ;
#25500=FACE_OUTER_BOUND ( 'NONE', #27222, .T. ) ;
#25501=CARTESIAN_POINT ( 'NONE',  ( -0.07097307671285064956, -0.2545179073170276141, -0.04495255068434172996 ) ) ;
#25512=EDGE_CURVE ( 'NONE', #16719, #752, #5699, .T. ) ;
#25562=VERTEX_POINT ( 'NONE', #45942 ) ;
#25568=CARTESIAN_POINT ( 'NONE',  ( -0.1711365707896517763, 0.1966896243421524526, -0.3121915932859947174 ) ) ;
#25591=CARTESIAN_POINT ( 'NONE',  ( -0.2559055118110235005, 0.1248284115715151549, -0.08765918451895586549 ) ) ;
#25605=DIRECTION ( 'NONE',  ( 0.000000000000000000, 0.000000000000000000, 1.000000000000000000 ) ) ;
#25675=ADVANCED_FACE ( 'NONE', ( #36595 ), #47376, .F. ) ;
#25689=ORIENTED_EDGE ( 'NONE', *, *, #31097, .T. ) ;
#25692=CARTESIAN_POINT ( 'NONE',  ( 0.000000000000000000, 0.000000000000000000, 0.000000000000000000 ) ) ;
#25714=EDGE_CURVE ( 'NONE', #21602, #19657, #19352, .T. ) ;
#25732=CARTESIAN_POINT ( 'NONE',  ( -0.1939037905414077168, -0.1835438265964373927, -0.05114647357133220162 ) ) ;
#25786=DIRECTION ( 'NONE',  ( 1.000000000000000000, 0.000000000000000000, 0.000000000000000000 ) ) ;
#25851=DIRECTION ( 'NONE',  ( 1.000000000000000000, 0.000000000000000000, 0.000000000000000000 ) ) ;
#25953=CARTESIAN_POINT ( 'NONE',  ( -0.2559055118110236116, -0.1477471161312049197, -0.1122047244094488277 ) ) ;
#26026=CARTESIAN_POINT ( 'NONE',  ( -0.2559055118110236116, -0.05426249550635786623, -0.03952467149259050738 ) ) ;
#26039=ADVANCED_FACE ( 'NONE', ( #13319 ), #24107, .F. ) ;
#26052=AXIS2_PLACEMENT_3D ( 'NONE', #6164, #31134, #31369 ) ;
#26056=CIRCLE ( 'NONE', #30654, 0.1574803149606299191 ) ;
#26088=CARTESIAN_POINT ( 'NONE',  ( 0.2559043144403723158, -0.05922267293569646873, -0.04185085927340410905 ) ) ;
#26090=EDGE_CURVE ( 'NONE', #43509, #9873, #14786, .T. ) ;
#26104=LINE ( 'NONE', #32177, #6901 ) ;
#26137=CARTESIAN_POINT ( 'NONE',  ( -0.05814395269903865904, -0.2619241685425540700, -0.3078067560681180259 ) ) ;
#26163=ORIENTED_EDGE ( 'NONE', *, *, #26287, .F. ) ;
#26164=SURFACE_SIDE_STYLE ('',( #43875 ) ) ;
#26167=CARTESIAN_POINT ( 'NONE',  ( 0.2341188618547038192, 0.1603256443482194427, -0.2993662881638891604 ) ) ;
#26188=CONICAL_SURFACE ( 'NONE', #2414, 0.1377952755905513804, 0.9599310885968808105 ) ;
#26199=CARTESIAN_POINT ( 'NONE',  ( -0.05642593091638983815, -0.2629167058585551442, -0.05524818609633137811 ) ) ;
#26234=DIRECTION ( 'NONE',  ( 0.000000000000000000, 0.000000000000000000, 1.000000000000000000 ) ) ;
#26238=FACE_OUTER_BOUND ( 'NONE', #27086, .T. ) ;
#26277=ADVANCED_FACE ( 'NONE', ( #32958 ), #14141, .F. ) ;
#26287=EDGE_CURVE ( 'NONE', #26963, #30980, #39865, .T. ) ;
#26322=ORIENTED_EDGE ( 'NONE', *, *, #46789, .T. ) ;
#26340=ORIENTED_EDGE ( 'NONE', *, *, #8755, .T. ) ;
#26396=CARTESIAN_POINT ( 'NONE',  ( -0.2559118981538488491, 0.03129849267415509700, -0.3138669400184891378 ) ) ;
#26398=AXIS2_PLACEMENT_3D ( 'NONE', #32773, #33007, #26518 ) ;
#26400=AXIS2_PLACEMENT_3D ( 'NONE', #1473, #41952, #9159 ) ;
#26416=ORIENTED_EDGE ( 'NONE', *, *, #18459, .F. ) ;
#26458=EDGE_CURVE ( 'NONE', #7920, #28768, #30256, .T. ) ;
#26518=DIRECTION ( 'NONE',  ( 1.000000000000000000, 0.000000000000000000, 0.000000000000000000 ) ) ;
#26543=DIRECTION ( 'NONE',  ( 0.8191520442889861364, 0.000000000000000000, 0.5735764363510541530 ) ) ;
#26580=VERTEX_POINT ( 'NONE', #32375 ) ;
#26583=AXIS2_PLACEMENT_3D ( 'NONE', #5238, #45480, #20099 ) ;
#26586=DIRECTION ( 'NONE',  ( -1.000000000000000000, 0.000000000000000000, 0.000000000000000000 ) ) ;
#26588=CARTESIAN_POINT ( 'NONE',  ( -0.1377952755905509363, 0.000000000000000000, -0.1436967020037460685 ) ) ;
#26633=DIRECTION ( 'NONE',  ( 1.000000000000000000, 0.000000000000000000, 0.000000000000000000 ) ) ;
#26651=AXIS2_PLACEMENT_3D ( 'NONE', #29055, #14167, #43373 ) ;
#26652=CARTESIAN_POINT ( 'NONE',  ( 0.05652825169351837625, 0.2628576309303346514, -0.05517042925146131011 ) ) ;
#26655=CARTESIAN_POINT ( 'NONE',  ( 0.1377952755905512694, 0.000000000000000000, -0.3149606299212598381 ) ) ;
#26677=DIRECTION ( 'NONE',  ( 0.000000000000000000, 0.000000000000000000, 1.000000000000000000 ) ) ;
#26709=DIRECTION ( 'NONE',  ( 0.000000000000000000, 0.000000000000000000, 1.000000000000000000 ) ) ;
#26713=FACE_OUTER_BOUND ( 'NONE', #210, .T. ) ;
#26714=ORIENTED_EDGE ( 'NONE', *, *, #20832, .F. ) ;
#26751=ORIENTED_EDGE ( 'NONE', *, *, #8755, .F. ) ;
#26768=CARTESIAN_POINT ( 'NONE',  ( 0.1574803149606299191, 0.000000000000000000, -0.3149606299212598381 ) ) ;
#26806=CARTESIAN_POINT ( 'NONE',  ( 0.2559054582636642317, -0.08442141331286162620, -0.05646086002838572593 ) ) ;
#26853=CARTESIAN_POINT ( 'NONE',  ( -0.06073293532415852819, -0.2604299181697397603, -0.3083162604245307525 ) ) ;
#26859=AXIS2_PLACEMENT_3D ( 'NONE', #28158, #39144, #35110 ) ;
#26861=CYLINDRICAL_SURFACE ( 'NONE', #1540, 0.1377952755905511306 ) ;
#26869=EDGE_CURVE ( 'NONE', #28934, #3606, #14854, .T. ) ;
#26892=DIRECTION ( 'NONE',  ( -0.000000000000000000, -0.000000000000000000, -1.000000000000000000 ) ) ;
#26918=VERTEX_POINT ( 'NONE', #42107 ) ;
#26949=CIRCLE ( 'NONE', #5514, 0.1574803149606299191 ) ;
#26963=VERTEX_POINT ( 'NONE', #15810 ) ;
#27007=LINE ( 'NONE', #34194, #33286 ) ;
#27018=AXIS2_PLACEMENT_3D ( 'NONE', #8580, #41380, #44987 ) ;
#27050=CARTESIAN_POINT ( 'NONE',  ( 0.2559054708194526406, -0.07549683194480610871, -0.05060588599970165802 ) ) ;
#27086=EDGE_LOOP ( 'NONE', ( #14222, #32136, #30114, #28793, #357, #23118, #15815 ) ) ;
#27094=EDGE_CURVE ( 'NONE', #28164, #40149, #42695, .T. ) ;
#27107=CARTESIAN_POINT ( 'NONE',  ( 0.05036568513383885698, 0.2664124483477642302, -0.3061783854718803100 ) ) ;
#27146=ORIENTED_EDGE ( 'NONE', *, *, #11179, .F. ) ;
#27192=DIRECTION ( 'NONE',  ( 1.000000000000000000, 0.000000000000000000, 0.000000000000000000 ) ) ;
#27196=EDGE_CURVE ( 'NONE', #3799, #25562, #2153, .T. ) ;
#27201=DIRECTION ( 'NONE',  ( -0.8191520442889798082, 1.003171929053510079E-16, 0.5735764363510631458 ) ) ;
#27204=DIRECTION ( 'NONE',  ( -1.000000000000000000, 0.000000000000000000, 0.000000000000000000 ) ) ;
#27222=EDGE_LOOP ( 'NONE', ( #23645, #27937, #32117, #31046 ) ) ;
#27224=FACE_OUTER_BOUND ( 'NONE', #13168, .T. ) ;
#27235=ORIENTED_EDGE ( 'NONE', *, *, #43324, .F. ) ;
#27256=CARTESIAN_POINT ( 'NONE',  ( -0.1578366172103670140, -0.2043672459941665021, -0.3136338785705618526 ) ) ;
#27259=LINE ( 'NONE', #4692, #39839 ) ;
#27316=CARTESIAN_POINT ( 'NONE',  ( 0.1377952755905509641, 1.687505431895956722E-17, -0.2219368594840610276 ) ) ;
#27321=DIRECTION ( 'NONE',  ( -1.000000000000000000, 0.000000000000000000, 0.000000000000000000 ) ) ;
#27367=EDGE_CURVE ( 'NONE', #13443, #15682, #40412, .T. ) ;
#27377=CARTESIAN_POINT ( 'NONE',  ( 0.08568752866847809124, 0.2460225145194667729, -0.03726912461315685238 ) ) ;
#27387=EDGE_LOOP ( 'NONE', ( #45965, #30422, #920, #36753 ) ) ;
#27404=FACE_OUTER_BOUND ( 'NONE', #5927, .T. ) ;
#27440=CYLINDRICAL_SURFACE ( 'NONE', #13827, 0.1377952755905510751 ) ;
#27441=DIRECTION ( 'NONE',  ( 0.000000000000000000, 0.000000000000000000, 1.000000000000000000 ) ) ;
#27459=CARTESIAN_POINT ( 'NONE',  ( 0.1496320939568084596, 0.2091027599425386019, -0.3142669362052408211 ) ) ;
#27526=DIRECTION ( 'NONE',  ( 0.000000000000000000, 0.000000000000000000, 1.000000000000000000 ) ) ;
#27556=CARTESIAN_POINT ( 'NONE',  ( 0.000000000000000000, 0.000000000000000000, -0.04012007874015743186 ) ) ;
#27564=ORIENTED_EDGE ( 'NONE', *, *, #18438, .T. ) ;
#27639=EDGE_LOOP ( 'NONE', ( #19222, #46154, #26322 ) ) ;
#27656=CARTESIAN_POINT ( 'NONE',  ( -0.1089815878282069106, 0.2325720113816387991, -0.3144321013757216399 ) ) ;
#27714=ORIENTED_EDGE ( 'NONE', *, *, #41797, .F. ) ;
#27717=CIRCLE ( 'NONE', #37632, 0.1377952755905509641 ) ;
#27727=CARTESIAN_POINT ( 'NONE',  ( -0.1528603379500407256, 0.2072402749985339798, -0.03001342526389673415 ) ) ;
#27741=ORIENTED_EDGE ( 'NONE', *, *, #7200, .T. ) ;
#27777=DIRECTION ( 'NONE',  ( 0.000000000000000000, 0.000000000000000000, 1.000000000000000000 ) ) ;
#27782=DIRECTION ( 'NONE',  ( 0.000000000000000000, 0.000000000000000000, 1.000000000000000000 ) ) ;
#27790=AXIS2_PLACEMENT_3D ( 'NONE', #1218, #16342, #15869 ) ;
#27810=CARTESIAN_POINT ( 'NONE',  ( 0.000000000000000000, 0.000000000000000000, -0.3001770169643759867 ) ) ;
#27823=B_SPLINE_CURVE_WITH_KNOTS ( 'NONE', 3,
 ( #1194, #33593, #44560, #11779, #22773, #26396, #951, #15610, #4358, #12307, #15669, #45687, #2555, #16954, #41852, #1855, #23449 ),
 .UNSPECIFIED., .F., .F.,
 ( 4, 2, 2, 2, 2, 1, 2, 2, 4 ),
 ( 0.000000000000000000, 0.1249999999999997502, 0.1874999999999995837, 0.2499999999999993894, 0.3749999999999990563, 0.4374999999999988343, 0.4687499999999987232, 0.4999999999999986122, 1.000000000000000000 ),
 .UNSPECIFIED. ) ;
#27828=CARTESIAN_POINT ( 'NONE',  ( 0.2559053678971339174, 0.03992796258515165370, -0.03403288757427402195 ) ) ;
#27872=APPLICATION_CONTEXT ( 'automotive_design' ) ;
#27874=CIRCLE ( 'NONE', #34776, 0.1377952755905509363 ) ;
#27877=ORIENTED_EDGE ( 'NONE', *, *, #42984, .T. ) ;
#27903=CARTESIAN_POINT ( 'NONE',  ( 0.2559055118110236116, 0.06940437565852064505, -0.3096270012539200644 ) ) ;
#27907=CARTESIAN_POINT ( 'NONE',  ( -0.1377952755905511306, 1.687505431895958263E-17, -0.3149606299212598381 ) ) ;
#27908=CARTESIAN_POINT ( 'NONE',  ( 0.1631814734428348734, -0.2012842543237225446, -0.3131151337379049493 ) ) ;
#27918=VECTOR ( 'NONE', #21110, 39.37007874015748854 ) ;
#27922=DIRECTION ( 'NONE',  ( 0.000000000000000000, 0.000000000000000000, 1.000000000000000000 ) ) ;
#27925=ORIENTED_EDGE ( 'NONE', *, *, #42442, .T. ) ;
#27937=ORIENTED_EDGE ( 'NONE', *, *, #45312, .T. ) ;
#27939=CARTESIAN_POINT ( 'NONE',  ( -0.2559055118110235005, -0.1351184156184602747, -0.2957496633320546020 ) ) ;
#27950=CARTESIAN_POINT ( 'NONE',  ( -0.09357655176633561389, 0.2414677849102764839, -0.03395687952545718702 ) ) ;
#27980=CIRCLE ( 'NONE', #5754, 0.1377952755905509363 ) ;
#28017=DIRECTION ( 'NONE',  ( 0.000000000000000000, 0.000000000000000000, 1.000000000000000000 ) ) ;
#28043=CARTESIAN_POINT ( 'NONE',  ( 0.1063536270747394152, 0.2340938383371280740, -0.3144333452974443222 ) ) ;
#28050=CARTESIAN_POINT ( 'NONE',  ( 0.2559052630942058038, 0.07638014557814261363, -0.05128389705078049282 ) ) ;
#28070=CARTESIAN_POINT ( 'NONE',  ( 0.08812199945789689348, 0.2446169721538616060, -0.03618545512906795603 ) ) ;
#28115=CARTESIAN_POINT ( 'NONE',  ( 0.2559055118110236671, -0.04912888505753350288, -0.3129193602642642014 ) ) ;
#28158=CARTESIAN_POINT ( 'NONE',  ( 0.000000000000000000, 0.000000000000000000, -0.07924015748031493223 ) ) ;
#28164=VERTEX_POINT ( 'NONE', #43470 ) ;
#28171=VECTOR ( 'NONE', #27441, 39.37007874015748143 ) ;
#28213=ORIENTED_EDGE ( 'NONE', *, *, #41797, .T. ) ;
#28234=CARTESIAN_POINT ( 'NONE',  ( -0.2559055118110236116, 0.03045100533025396627, -0.03118462788502844932 ) ) ;
#28248=CARTESIAN_POINT ( 'NONE',  ( 0.000000000000000000, 0.000000000000000000, -0.3149606299212598381 ) ) ;
#28258=DIRECTION ( 'NONE',  ( 0.000000000000000000, 0.000000000000000000, 1.000000000000000000 ) ) ;
#28268=EDGE_CURVE ( 'NONE', #34984, #1339, #32832, .T. ) ;
#28273=CARTESIAN_POINT ( 'NONE',  ( 0.2559054998105182999, 0.08068256135019109820, -0.05400407908655117245 ) ) ;
#28278=EDGE_CURVE ( 'NONE', #31834, #40149, #14981, .T. ) ;
#28283=ORIENTED_EDGE ( 'NONE', *, *, #8326, .T. ) ;
#28328=ORIENTED_EDGE ( 'NONE', *, *, #43656, .T. ) ;
#28339=DIRECTION ( 'NONE',  ( 0.000000000000000000, 0.000000000000000000, 1.000000000000000000 ) ) ;
#28390=CARTESIAN_POINT ( 'NONE',  ( 0.2151545284320233176, -0.1712747073548132604, -0.06815351164857932909 ) ) ;
#28402=DIRECTION ( 'NONE',  ( 0.8191520442889989040, 1.003171929053533375E-16, -0.5735764363510359454 ) ) ;
#28410=CARTESIAN_POINT ( 'NONE',  ( -0.2001839496640346883, 0.1799179750364343355, -0.05578523004296902232 ) ) ;
#28429=DIRECTION ( 'NONE',  ( 0.8191520442889873577, 0.000000000000000000, 0.5735764363510523767 ) ) ;
#28433=EDGE_CURVE ( 'NONE', #22098, #24404, #9190, .T. ) ;
#28479=DIRECTION ( 'NONE',  ( 0.000000000000000000, 0.000000000000000000, 1.000000000000000000 ) ) ;
#28516=CARTESIAN_POINT ( 'NONE',  ( 0.2559055118110236116, 0.1477471161312045311, -0.1122047244094488277 ) ) ;
#28525=VERTEX_POINT ( 'NONE', #30333 ) ;
#28526=AXIS2_PLACEMENT_3D ( 'NONE', #5456, #34718, #26586 ) ;
#28534=AXIS2_PLACEMENT_3D ( 'NONE', #40166, #39937, #7125 ) ;
#28541=CARTESIAN_POINT ( 'NONE',  ( 0.1219373188186398949, -0.2250936884182059838, -0.02739586109245262593 ) ) ;
#28584=EDGE_LOOP ( 'NONE', ( #38310, #30833, #13558, #14594 ) ) ;
#28591=DIRECTION ( 'NONE',  ( 0.000000000000000000, 0.000000000000000000, -1.000000000000000000 ) ) ;
#28608=DIRECTION ( 'NONE',  ( -0.8191520442889980158, 0.000000000000000000, -0.5735764363510372776 ) ) ;
#28611=CARTESIAN_POINT ( 'NONE',  ( 0.2559055118110236116, 0.000000000000000000, -0.3149606299212598381 ) ) ;
#28615=EDGE_CURVE ( 'NONE', #31906, #21602, #23097, .T. ) ;
#28616=DIRECTION ( 'NONE',  ( 0.000000000000000000, 0.000000000000000000, 1.000000000000000000 ) ) ;
#28623=EDGE_CURVE ( 'NONE', #8606, #24988, #38957, .T. ) ;
#28660=CARTESIAN_POINT ( 'NONE',  ( -0.06699593397071766654, 0.2568141117498029535, -0.04769437235512034856 ) ) ;
#28687=ORIENTED_EDGE ( 'NONE', *, *, #26458, .T. ) ;
#28710=ADVANCED_FACE ( 'NONE', ( #9442 ), #24291, .F. ) ;
#28768=VERTEX_POINT ( 'NONE', #14215 ) ;
#28785=DIRECTION ( 'NONE',  ( -1.000000000000000000, 0.000000000000000000, 0.000000000000000000 ) ) ;
#28787=CARTESIAN_POINT ( 'NONE',  ( 0.1657445988168603501, -0.1998015435187681099, -0.03531881253561163642 ) ) ;
#28793=ORIENTED_EDGE ( 'NONE', *, *, #8159, .F. ) ;
#28849=CARTESIAN_POINT ( 'NONE',  ( 0.2559055118110236116, 0.09798266946487620144, -0.3050161490475334358 ) ) ;
#28852=CARTESIAN_POINT ( 'NONE',  ( 0.1377952755905509641, 0.000000000000000000, -0.2219368594840610276 ) ) ;
#28931=EDGE_LOOP ( 'NONE', ( #12569, #27741, #23133 ) ) ;
#28934=VERTEX_POINT ( 'NONE', #18267 ) ;
#28944=ADVANCED_FACE ( 'NONE', ( #19198 ), #8339, .F. ) ;
#28971=CARTESIAN_POINT ( 'NONE',  ( -4.999628824793424855E-17, -0.2954942322624090623, -0.3149606299212598381 ) ) ;
#29050=EDGE_CURVE ( 'NONE', #65, #25178, #8411, .T. ) ;
#29055=CARTESIAN_POINT ( 'NONE',  ( 0.000000000000000000, 0.000000000000000000, 2.731847993664263218E-16 ) ) ;
#29119=CARTESIAN_POINT ( 'NONE',  ( -0.05652825169351902851, -0.2628576309303358172, -0.05517042925146417587 ) ) ;
#29124=ORIENTED_EDGE ( 'NONE', *, *, #39152, .T. ) ;
#29163=VECTOR ( 'NONE', #6282, 39.37007874015748143 ) ;
#29179=EDGE_CURVE ( 'NONE', #6423, #13443, #976, .T. ) ;
#29195=ORIENTED_EDGE ( 'NONE', *, *, #24035, .T. ) ;
#29218=CARTESIAN_POINT ( 'NONE',  ( 0.1279527559055118058, -0.2216206741968047289, -0.3149606299212598381 ) ) ;
#29224=CARTESIAN_POINT ( 'NONE',  ( -0.2559055118110235560, 0.08067097267005921002, -0.05399682104008290962 ) ) ;
#29233=DIRECTION ( 'NONE',  ( 1.000000000000000000, 0.000000000000000000, 0.000000000000000000 ) ) ;
#29242=AXIS2_PLACEMENT_3D ( 'NONE', #8950, #19492, #8464 ) ;
#29246=ORIENTED_EDGE ( 'NONE', *, *, #42444, .T. ) ;
#29287=ORIENTED_EDGE ( 'NONE', *, *, #29563, .F. ) ;
#29348=CARTESIAN_POINT ( 'NONE',  ( 0.000000000000000000, 0.000000000000000000, -0.01478361295688420882 ) ) ;
#29412=CARTESIAN_POINT ( 'NONE',  ( 0.000000000000000000, 0.000000000000000000, -0.2357204724409448504 ) ) ;
#29426=ORIENTED_EDGE ( 'NONE', *, *, #39349, .F. ) ;
#29469=CARTESIAN_POINT ( 'NONE',  ( -0.1574803149606299191, 0.000000000000000000, -0.1574803149606298636 ) ) ;
#29528=DIRECTION ( 'NONE',  ( 1.000000000000000000, 0.000000000000000000, 0.000000000000000000 ) ) ;
#29536=DIRECTION ( 'NONE',  ( -0.8191520442889873577, 1.003171929053519323E-16, 0.5735764363510523767 ) ) ;
#29545=ORIENTED_EDGE ( 'NONE', *, *, #44394, .T. ) ;
#29554=CIRCLE ( 'NONE', #39434, 0.1574803149606299191 ) ;
#29563=EDGE_CURVE ( 'NONE', #23841, #4869, #45861, .T. ) ;
#29578=DIRECTION ( 'NONE',  ( 1.000000000000000000, 0.000000000000000000, 0.000000000000000000 ) ) ;
#29580=AXIS2_PLACEMENT_3D ( 'NONE', #13146, #27782, #42342 ) ;
#29600=CARTESIAN_POINT ( 'NONE',  ( -0.1339681929923939863, -0.2181476599754015588, -0.02739586109245887441 ) ) ;
#29622=DIRECTION ( 'NONE',  ( 0.000000000000000000, 0.000000000000000000, -1.000000000000000000 ) ) ;
#29635=DIRECTION ( 'NONE',  ( 0.8191520442889996811, 1.003171929053534361E-16, -0.5735764363510347241 ) ) ;
#29641=DIRECTION ( 'NONE',  ( 1.000000000000000000, 0.000000000000000000, 0.000000000000000000 ) ) ;
#29671=CARTESIAN_POINT ( 'NONE',  ( -0.1738065908856299691, 0.1951474930449461631, -0.3118411609179210786 ) ) ;
#29699=CARTESIAN_POINT ( 'NONE',  ( 0.1574803149606299191, 0.000000000000000000, -0.3139606299212599483 ) ) ;
#29713=CARTESIAN_POINT ( 'NONE',  ( 0.000000000000000000, 0.000000000000000000, -0.02633646578327370619 ) ) ;
#29810=VECTOR ( 'NONE', #29635, 39.37007874015748854 ) ;
#29812=ORIENTED_EDGE ( 'NONE', *, *, #43210, .F. ) ;
#29832=ORIENTED_EDGE ( 'NONE', *, *, #45634, .T. ) ;
#29857=CARTESIAN_POINT ( 'NONE',  ( -0.05734381846710268071, 0.2623867632340645129, -0.05455490385610123338 ) ) ;
#29884=EDGE_CURVE ( 'NONE', #43008, #18573, #3024, .T. ) ;
#29951=VECTOR ( 'NONE', #36273, 39.37007874015748143 ) ;
#29955=CARTESIAN_POINT ( 'NONE',  ( 0.000000000000000000, 0.000000000000000000, -0.0004999999999998990712 ) ) ;
#29963=EDGE_CURVE ( 'NONE', #31750, #43509, #5245, .T. ) ;
#29990=AXIS2_PLACEMENT_3D ( 'NONE', #30047, #43904, #23047 ) ;
#30017=VERTEX_POINT ( 'NONE', #45963 ) ;
#30023=EDGE_LOOP ( 'NONE', ( #10646, #13084, #39379, #18641 ) ) ;
#30025=( NAMED_UNIT ( * ) PLANE_ANGLE_UNIT ( ) SI_UNIT ( $, .RADIAN. ) ) ;
#30040=CARTESIAN_POINT ( 'NONE',  ( 0.000000000000000000, 0.000000000000000000, -0.2219368594840610276 ) ) ;
#30047=CARTESIAN_POINT ( 'NONE',  ( 0.000000000000000000, 0.000000000000000000, -0.1574803149606298636 ) ) ;
#30061=ADVANCED_FACE ( 'NONE', ( #3774 ), #21275, .F. ) ;
#30073=ORIENTED_EDGE ( 'NONE', *, *, #23275, .F. ) ;
#30111=DIRECTION ( 'NONE',  ( -0.8191520442889873577, 1.003171929053519323E-16, 0.5735764363510523767 ) ) ;
#30114=ORIENTED_EDGE ( 'NONE', *, *, #23101, .T. ) ;
#30140=CARTESIAN_POINT ( 'NONE',  ( 3.127876812047771422E-16, 0.2954942322624074524, -0.3149606299212598381 ) ) ;
#30152=CONICAL_SURFACE ( 'NONE', #4068, 0.1574803149606299191, 0.9599310885968603824 ) ;
#30168=DIMENSIONAL_EXPONENTS ( 1.000000000000000000, 0.000000000000000000, 0.000000000000000000, 0.000000000000000000, 0.000000000000000000, 0.000000000000000000, 0.000000000000000000 ) ;
#30193=CARTESIAN_POINT ( 'NONE',  ( 0.2559046719760603161, -0.09147515633630175225, -0.06132792317783448272 ) ) ;
#30219=FACE_OUTER_BOUND ( 'NONE', #33412, .T. ) ;
#30221=FACE_OUTER_BOUND ( 'NONE', #16855, .T. ) ;
#30232=CARTESIAN_POINT ( 'NONE',  ( -0.02156745609633855046, -0.2830359600832498268, -0.2989494884453736123 ) ) ;
#30250=ADVANCED_FACE ( 'NONE', ( #15282 ), #9170, .F. ) ;
#30252=ORIENTED_EDGE ( 'NONE', *, *, #33079, .F. ) ;
#30256=CIRCLE ( 'NONE', #42433, 0.1377952755905511861 ) ;
#30265=CARTESIAN_POINT ( 'NONE',  ( 0.05614424849856877037, 0.2630793352783085681, -0.05546260682012606191 ) ) ;
#30271=DIRECTION ( 'NONE',  ( 0.000000000000000000, 0.000000000000000000, 1.000000000000000000 ) ) ;
#30273=FACE_OUTER_BOUND ( 'NONE', #34518, .T. ) ;
#30279=VECTOR ( 'NONE', #11239, 39.37007874015748143 ) ;
#30294=EDGE_CURVE ( 'NONE', #1846, #3412, #19335, .T. ) ;
#30295=CARTESIAN_POINT ( 'NONE',  ( 0.000000000000000000, 0.000000000000000000, -0.3149606299212598381 ) ) ;
#30333=CARTESIAN_POINT ( 'NONE',  ( 4.268512490100409430E-16, 0.2954942322624074524, -0.2921040715117803055 ) ) ;
#30402=DIRECTION ( 'NONE',  ( 0.000000000000000000, 0.000000000000000000, 1.000000000000000000 ) ) ;
#30422=ORIENTED_EDGE ( 'NONE', *, *, #26458, .F. ) ;
#30423=CARTESIAN_POINT ( 'NONE',  ( 0.000000000000000000, 0.000000000000000000, -0.07924015748031493223 ) ) ;
#30448=DIRECTION ( 'NONE',  ( 1.000000000000000000, 0.000000000000000000, 0.000000000000000000 ) ) ;
#30459=CARTESIAN_POINT ( 'NONE',  ( -0.07407796729095041111, -0.2527247573021067506, -0.3106979152243043996 ) ) ;
#30462=CARTESIAN_POINT ( 'NONE',  ( 0.01090721357323628377, 0.2891969495697860881, -0.2957398093695285390 ) ) ;
#30483=CARTESIAN_POINT ( 'NONE',  ( 0.2559055118110236116, 0.1477471161312045311, -0.2921040715117803055 ) ) ;
#30514=FACE_OUTER_BOUND ( 'NONE', #46244, .T. ) ;
#30519=CARTESIAN_POINT ( 'NONE',  ( -0.2559055118110235560, -0.1362856811059252049, -0.09992972387952742119 ) ) ;
#30521=DIRECTION ( 'NONE',  ( 1.000000000000000000, 0.000000000000000000, 0.000000000000000000 ) ) ;
#30531=CARTESIAN_POINT ( 'NONE',  ( -0.02178664995562274928, 0.2829157040457837557, -0.2993662881636575679 ) ) ;
#30554=DIRECTION ( 'NONE',  ( 0.8191520442889873577, 0.000000000000000000, 0.5735764363510523767 ) ) ;
#30588=CARTESIAN_POINT ( 'NONE',  ( -0.1377952755905510196, 1.687505431895957647E-17, -0.1828167807439035619 ) ) ;
#30591=ORIENTED_EDGE ( 'NONE', *, *, #21119, .F. ) ;
#30594=CARTESIAN_POINT ( 'NONE',  ( -0.2559077310846238351, -0.04350174606802800076, -0.3128500747680653116 ) ) ;
#30596=DIRECTION ( 'NONE',  ( 1.000000000000000000, 0.000000000000000000, 0.000000000000000000 ) ) ;
#30613=DIRECTION ( 'NONE',  ( 0.8191520442889873577, 0.000000000000000000, 0.5735764363510523767 ) ) ;
#30645=CARTESIAN_POINT ( 'NONE',  ( 0.2559055150599270911, -0.04346181788127674583, -0.03525533988057383966 ) ) ;
#30654=AXIS2_PLACEMENT_3D ( 'NONE', #5437, #27526, #38751 ) ;
#30721=CARTESIAN_POINT ( 'NONE',  ( -0.1574803149606299191, 0.000000000000000000, -0.2357204724409448504 ) ) ;
#30723=AXIS2_PLACEMENT_3D ( 'NONE', #21309, #3347, #36651 ) ;
#30748=AXIS2_PLACEMENT_3D ( 'NONE', #7876, #664, #15319 ) ;
#30759=FACE_OUTER_BOUND ( 'NONE', #19117, .T. ) ;
#30774=CARTESIAN_POINT ( 'NONE',  ( -0.07669050334325228091, 0.2512157378947911801, -0.3110703821945135505 ) ) ;
#30779=DIRECTION ( 'NONE',  ( 0.000000000000000000, 0.000000000000000000, 1.000000000000000000 ) ) ;
#30787=DIRECTION ( 'NONE',  ( 1.000000000000000000, 0.000000000000000000, 0.000000000000000000 ) ) ;
#30791=CIRCLE ( 'NONE', #3208, 0.1377952755905511861 ) ;
#30792=AXIS2_PLACEMENT_3D ( 'NONE', #29412, #4389, #11857 ) ;
#30800=DIRECTION ( 'NONE',  ( 1.000000000000000000, 0.000000000000000000, 0.000000000000000000 ) ) ;
#30812=CARTESIAN_POINT ( 'NONE',  ( 0.1832342603884100363, 0.1897030460626166204, -0.3104511204119947965 ) ) ;
#30833=ORIENTED_EDGE ( 'NONE', *, *, #36586, .T. ) ;
#30835=AXIS2_PLACEMENT_3D ( 'NONE', #29348, #41627, #43653 ) ;
#30837=CARTESIAN_POINT ( 'NONE',  ( -0.2558995472165326857, -0.1045113733907631348, -0.3031500423883560225 ) ) ;
#30854=AXIS2_PLACEMENT_3D ( 'NONE', #4580, #30975, #11813 ) ;
#30861=AXIS2_PLACEMENT_3D ( 'NONE', #34481, #38546, #1635 ) ;
#30925=ORIENTED_EDGE ( 'NONE', *, *, #46234, .F. ) ;
#30937=EDGE_CURVE ( 'NONE', #5631, #2951, #43007, .T. ) ;
#30955=VECTOR ( 'NONE', #8341, 39.37007874015748143 ) ;
#30957=CARTESIAN_POINT ( 'NONE',  ( 0.08080321177261283461, 0.2488424761941021024, -0.03960523631943477924 ) ) ;
#30960=ORIENTED_EDGE ( 'NONE', *, *, #7200, .F. ) ;
#30975=DIRECTION ( 'NONE',  ( 0.000000000000000000, 0.000000000000000000, 1.000000000000000000 ) ) ;
#30980=VERTEX_POINT ( 'NONE', #3724 ) ;
#30999=CARTESIAN_POINT ( 'NONE',  ( -0.06453057165845259291, 0.2582375021999043785, -0.3090319486758607015 ) ) ;
#31023=LINE ( 'NONE', #12810, #38857 ) ;
#31046=ORIENTED_EDGE ( 'NONE', *, *, #42442, .F. ) ;
#31054=ORIENTED_EDGE ( 'NONE', *, *, #26287, .T. ) ;
#31097=EDGE_CURVE ( 'NONE', #16796, #38700, #26104, .T. ) ;
#31128=FACE_OUTER_BOUND ( 'NONE', #44199, .T. ) ;
#31134=DIRECTION ( 'NONE',  ( 0.000000000000000000, 0.000000000000000000, 1.000000000000000000 ) ) ;
#31155=DIRECTION ( 'NONE',  ( 0.000000000000000000, 0.000000000000000000, 1.000000000000000000 ) ) ;
#31165=CARTESIAN_POINT ( 'NONE',  ( 0.07407796729086078835, 0.2527247573021684235, -0.3106979152242848596 ) ) ;
#31176=CONICAL_SURFACE ( 'NONE', #26583, 0.1574803149606299191, 0.9599310885968713736 ) ;
#31178=ORIENTED_EDGE ( 'NONE', *, *, #6931, .T. ) ;
#31218=ORIENTED_EDGE ( 'NONE', *, *, #41599, .F. ) ;
#31303=CARTESIAN_POINT ( 'NONE',  ( 0.000000000000000000, 0.000000000000000000, -0.3149606299212598381 ) ) ;
#31346=CYLINDRICAL_SURFACE ( 'NONE', #38617, 0.1377952755905511306 ) ;
#31348=CARTESIAN_POINT ( 'NONE',  ( 0.000000000000000000, 0.000000000000000000, -0.06545654452343109553 ) ) ;
#31351=ADVANCED_FACE ( 'NONE', ( #39579 ), #35256, .F. ) ;
#31353=EDGE_CURVE ( 'NONE', #18699, #873, #46067, .T. ) ;
#31369=DIRECTION ( 'NONE',  ( 1.000000000000000000, 0.000000000000000000, 0.000000000000000000 ) ) ;
#31383=ORIENTED_EDGE ( 'NONE', *, *, #10237, .T. ) ;
#31403=AXIS2_PLACEMENT_3D ( 'NONE', #7598, #8304, #44018 ) ;
#31432=CONICAL_SURFACE ( 'NONE', #18, 0.1574803149606299191, 0.9599310885968735940 ) ;
#31435=VERTEX_POINT ( 'NONE', #40045 ) ;
#31471=CARTESIAN_POINT ( 'NONE',  ( 0.2559055118110236116, -0.07734300567387089598, -0.3083604012389705717 ) ) ;
#31480=CARTESIAN_POINT ( 'NONE',  ( 0.000000000000000000, 0.000000000000000000, -0.04012007874015743186 ) ) ;
#31506=CARTESIAN_POINT ( 'NONE',  ( 0.1279527559055118058, 0.2216206741968047289, -0.3149606299212598381 ) ) ;
#31507=CARTESIAN_POINT ( 'NONE',  ( -0.02440571223931113296, -0.2814035877312771605, -0.08364281214758069460 ) ) ;
#31520=CARTESIAN_POINT ( 'NONE',  ( 0.1377952755905511861, 0.000000000000000000, -0.01478361295688420882 ) ) ;
#31530=CARTESIAN_POINT ( 'NONE',  ( -0.2559027535725037494, -0.08943520109415376007, -0.3062076317311127061 ) ) ;
#31535=CIRCLE ( 'NONE', #30792, 0.1574803149606299191 ) ;
#31541=CARTESIAN_POINT ( 'NONE',  ( -0.1660477163176994342, 0.1996265385480609222, -0.03544556188504487115 ) ) ;
#31572=VERTEX_POINT ( 'NONE', #34030 ) ;
#31584=ORIENTED_EDGE ( 'NONE', *, *, #34875, .F. ) ;
#31591=DIRECTION ( 'NONE',  ( -0.8191520442890534159, 0.000000000000000000, -0.5735764363509581187 ) ) ;
#31604=LINE ( 'NONE', #27316, #17694 ) ;
#31618=ADVANCED_FACE ( 'NONE', ( #41389 ), #23025, .F. ) ;
#31627=DIRECTION ( 'NONE',  ( -1.000000000000000000, -3.552713678800500140E-15, 0.000000000000000000 ) ) ;
#31642=CARTESIAN_POINT ( 'NONE',  ( 0.2559054633625183484, 0.04128200529817901976, -0.03449252736539545894 ) ) ;
#31690=DIRECTION ( 'NONE',  ( -1.000000000000000000, 0.000000000000000000, 0.000000000000000000 ) ) ;
#31731=CARTESIAN_POINT ( 'NONE',  ( -0.1574803149606299191, 1.928577636452524610E-17, -0.1183602362204724257 ) ) ;
#31750=VERTEX_POINT ( 'NONE', #38303 ) ;
#31773=CARTESIAN_POINT ( 'NONE',  ( -0.2031507276427601261, 0.1782051049717913449, -0.05809220732314908375 ) ) ;
#31774=B_SPLINE_CURVE_WITH_KNOTS ( 'NONE', 3,
 ( #31506, #23367, #12827, #5854, #27459, #2243, #2016, #37975, #34388, #34868, #30812, #37396, #7692, #34079, #4798, #26167, #30483 ),
 .UNSPECIFIED., .F., .F.,
 ( 4, 2, 2, 2, 2, 1, 2, 2, 4 ),
 ( 0.000000000000000000, 0.1250000000000009714, 0.1875000000000012768, 0.2500000000000012768, 0.3750000000000014433, 0.4375000000000018874, 0.4687500000000020539, 0.5000000000000021094, 1.000000000000000000 ),
 .UNSPECIFIED. ) ;
#31785=EDGE_CURVE ( 'NONE', #6423, #3799, #34480, .T. ) ;
#31797=CARTESIAN_POINT ( 'NONE',  ( -0.2431102362204724532, 0.000000000000000000, 0.000000000000000000 ) ) ;
#31811=CYLINDRICAL_SURFACE ( 'NONE', #46587, 0.1377952755905510751 ) ;
#31834=VERTEX_POINT ( 'NONE', #23164 ) ;
#31872=CARTESIAN_POINT ( 'NONE',  ( 0.2559030184365650995, 0.02510022111087184885, -0.02997901531815388293 ) ) ;
#31894=CARTESIAN_POINT ( 'NONE',  ( 0.05734381846710276398, -0.2623867632340661782, -0.05455490385610432119 ) ) ;
#31897=CARTESIAN_POINT ( 'NONE',  ( 0.1623289600446794489, 0.2017735634833385805, -0.03395687952545685395 ) ) ;
#31906=VERTEX_POINT ( 'NONE', #19323 ) ;
#31931=EDGE_CURVE ( 'NONE', #23841, #19150, #27259, .T. ) ;
#31933=ADVANCED_FACE ( 'NONE', ( #1571, #33972 ), #23634, .T. ) ;
#31958=CARTESIAN_POINT ( 'NONE',  ( 0.1495543973312418728, -0.2091518620004978180, -0.3144333452974441556 ) ) ;
#31969=CARTESIAN_POINT ( 'NONE',  ( -0.1377952755905509641, 1.687505431895957030E-17, -0.2219368594840610276 ) ) ;
#32002=CARTESIAN_POINT ( 'NONE',  ( -0.1574803149606299191, 1.928577636452524610E-17, -0.3139606299212599483 ) ) ;
#32012=LINE ( 'NONE', #46604, #4365 ) ;
#32039=FACE_OUTER_BOUND ( 'NONE', #19136, .T. ) ;
#32064=CARTESIAN_POINT ( 'NONE',  ( -0.2559055118110235560, 0.07633542835890737288, -0.05125767443128528833 ) ) ;
#32088=ORIENTED_EDGE ( 'NONE', *, *, #15366, .T. ) ;
#32117=ORIENTED_EDGE ( 'NONE', *, *, #41719, .T. ) ;
#32136=ORIENTED_EDGE ( 'NONE', *, *, #3197, .F. ) ;
#32162=CARTESIAN_POINT ( 'NONE',  ( 0.000000000000000000, 0.000000000000000000, -0.2748405511811023438 ) ) ;
#32168=FACE_OUTER_BOUND ( 'NONE', #14288, .T. ) ;
#32177=CARTESIAN_POINT ( 'NONE',  ( 0.1574803149606299191, 0.000000000000000000, -0.0009999999999999347518 ) ) ;
#32191=CARTESIAN_POINT ( 'NONE',  ( -2.680625843783058887E-15, -0.2954942322624074524, -0.2921040715117803055 ) ) ;
#32210=DIRECTION ( 'NONE',  ( 0.8191520442889991260, 1.003171929053533745E-16, -0.5735764363510356123 ) ) ;
#32214=UNCERTAINTY_MEASURE_WITH_UNIT (LENGTH_MEASURE( 1.000000000000000082E-05 ), #35928, 'distance_accuracy_value', 'NONE') ;
#32232=AXIS2_PLACEMENT_3D ( 'NONE', #28248, #17675, #25109 ) ;
#32244=CARTESIAN_POINT ( 'NONE',  ( -0.09118578515492140046, 0.2428480946569460674, -0.03489849683095607585 ) ) ;
#32289=CARTESIAN_POINT ( 'NONE',  ( -4.999628824793424855E-17, -0.2954942322624090623, -0.3149606299212598381 ) ) ;
#32297=VECTOR ( 'NONE', #24012, 39.37007874015748143 ) ;
#32313=CARTESIAN_POINT ( 'NONE',  ( -0.2559055118110236116, 0.03676409477166151657, -0.03301314027812374957 ) ) ;
#32314=AXIS2_PLACEMENT_3D ( 'NONE', #14436, #6752, #21374 ) ;
#32323=ORIENTED_EDGE ( 'NONE', *, *, #7379, .T. ) ;
#32325=FACE_OUTER_BOUND ( 'NONE', #6951, .T. ) ;
#32357=ORIENTED_EDGE ( 'NONE', *, *, #30294, .F. ) ;
#32372=CARTESIAN_POINT ( 'NONE',  ( 0.1377952755905510751, 0.000000000000000000, -0.3149606299212598381 ) ) ;
#32375=CARTESIAN_POINT ( 'NONE',  ( 0.1574803149606299191, 0.000000000000000000, 2.731847993664263218E-16 ) ) ;
#32393=ORIENTED_EDGE ( 'NONE', *, *, #33052, .F. ) ;
#32395=CONICAL_SURFACE ( 'NONE', #35424, 0.1377952755905509641, 0.9599310885968941331 ) ;
#32421=CARTESIAN_POINT ( 'NONE',  ( 0.000000000000000000, 0.000000000000000000, 0.000000000000000000 ) ) ;
#32450=EDGE_CURVE ( 'NONE', #9930, #31834, #1633, .T. ) ;
#32460=CARTESIAN_POINT ( 'NONE',  ( -0.04877781748286048186, -0.2673323462081961810, -0.06129781628410210792 ) ) ;
#32539=EDGE_CURVE ( 'NONE', #31906, #31572, #16961, .T. ) ;
#32540=ORIENTED_EDGE ( 'NONE', *, *, #1941, .T. ) ;
#32554=CARTESIAN_POINT ( 'NONE',  ( -0.2559055118110236116, 0.1477471161312031434, -0.3149606299212598381 ) ) ;
#32556=CARTESIAN_POINT ( 'NONE',  ( -0.2559055118110236116, 0.000000000000000000, -0.3149606299212598381 ) ) ;
#32560=DIRECTION ( 'NONE',  ( 0.000000000000000000, 0.000000000000000000, 1.000000000000000000 ) ) ;
#32652=DIRECTION ( 'NONE',  ( 0.000000000000000000, 0.000000000000000000, 1.000000000000000000 ) ) ;
#32673=ORIENTED_EDGE ( 'NONE', *, *, #15332, .T. ) ;
#32691=CARTESIAN_POINT ( 'NONE',  ( -0.1789895911306832177, -0.1921545436409667906, -0.04147023971061550990 ) ) ;
#32704=ORIENTED_EDGE ( 'NONE', *, *, #5522, .F. ) ;
#32724=CARTESIAN_POINT ( 'NONE',  ( -0.05712600390865770622, 0.2625125185280161588, -0.05471869868084688199 ) ) ;
#32748=EDGE_LOOP ( 'NONE', ( #36714, #8513, #14958, #41726, #36260 ) ) ;
#32767=ORIENTED_EDGE ( 'NONE', *, *, #28278, .T. ) ;
#32773=CARTESIAN_POINT ( 'NONE',  ( 0.000000000000000000, 0.000000000000000000, -0.1321438491773566926 ) ) ;
#32782=CARTESIAN_POINT ( 'NONE',  ( 0.1062722551331691384, -0.2341365745593732284, -0.3142669362052405435 ) ) ;
#32787=CARTESIAN_POINT ( 'NONE',  ( -0.2559055118110236116, 0.04268984771565554476, -0.03498110359409837417 ) ) ;
#32822=CARTESIAN_POINT ( 'NONE',  ( 0.000000000000000000, 0.000000000000000000, -0.1045766232635885612 ) ) ;
#32832=CIRCLE ( 'NONE', #3764, 0.1377952755905510474 ) ;
#32883=EDGE_CURVE ( 'NONE', #40149, #28164, #12378, .T. ) ;
#32891=DIRECTION ( 'NONE',  ( -1.000000000000000000, 0.000000000000000000, 0.000000000000000000 ) ) ;
#32900=AXIS2_PLACEMENT_3D ( 'NONE', #14868, #17972, #29528 ) ;
#32914=AXIS2_PLACEMENT_3D ( 'NONE', #24479, #39071, #35511 ) ;
#32928=CARTESIAN_POINT ( 'NONE',  ( -0.1982027233128455801, -0.1810618366036195193, -0.05428606100832154835 ) ) ;
#32958=FACE_OUTER_BOUND ( 'NONE', #21390, .T. ) ;
#32987=EDGE_LOOP ( 'NONE', ( #45129, #6387, #46205, #12473 ) ) ;
#33007=DIRECTION ( 'NONE',  ( 0.000000000000000000, 0.000000000000000000, 1.000000000000000000 ) ) ;
#33017=CARTESIAN_POINT ( 'NONE',  ( 0.09806891812721182933, -0.2388741431486400835, -0.3136338785705766741 ) ) ;
#33032=EDGE_CURVE ( 'NONE', #24404, #26580, #2379, .T. ) ;
#33052=EDGE_CURVE ( 'NONE', #7313, #43008, #15438, .T. ) ;
#33079=EDGE_CURVE ( 'NONE', #21785, #45855, #18472, .T. ) ;
#33083=EDGE_CURVE ( 'NONE', #25562, #3799, #42939, .T. ) ;
#33102=ORIENTED_EDGE ( 'NONE', *, *, #6931, .F. ) ;
#33165=CARTESIAN_POINT ( 'NONE',  ( 0.1377952755905511306, 0.000000000000000000, -0.3149606299212598381 ) ) ;
#33170=CARTESIAN_POINT ( 'NONE',  ( -0.1635016310872839662, -0.2010965215412215124, -0.03441347972012470668 ) ) ;
#33207=EDGE_CURVE ( 'NONE', #1339, #38506, #269, .T. ) ;
#33216=CARTESIAN_POINT ( 'NONE',  ( 0.000000000000000000, 0.000000000000000000, 0.000000000000000000 ) ) ;
#33224=ORIENTED_EDGE ( 'NONE', *, *, #37607, .F. ) ;
#33227=FACE_OUTER_BOUND ( 'NONE', #43183, .T. ) ;
#33286=VECTOR ( 'NONE', #33732, 39.37007874015748143 ) ;
#33292=DIRECTION ( 'NONE',  ( -1.000000000000000000, 0.000000000000000000, 0.000000000000000000 ) ) ;
#33341=CARTESIAN_POINT ( 'NONE',  ( -0.1171103306480026085, -0.2278805513378966141, -0.3149606299212598381 ) ) ;
#33347=FACE_OUTER_BOUND ( 'NONE', #40225, .T. ) ;
#33381=CARTESIAN_POINT ( 'NONE',  ( 0.000000000000000000, 0.000000000000000000, -0.2886241641379866385 ) ) ;
#33401=CARTESIAN_POINT ( 'NONE',  ( -0.1976644210311677141, -0.1813726255708516255, -0.05388431474956710543 ) ) ;
#33412=EDGE_LOOP ( 'NONE', ( #15528, #14893, #43606 ) ) ;
#33456=CARTESIAN_POINT ( 'NONE',  ( 0.2431102362204724532, 3.299925748462481561E-17, 0.000000000000000000 ) ) ;
#33477=ORIENTED_EDGE ( 'NONE', *, *, #998, .T. ) ;
#33490=CARTESIAN_POINT ( 'NONE',  ( 0.06863485658970966408, -0.2558675481226387327, -0.3097625555229703842 ) ) ;
#33500=AXIS2_PLACEMENT_3D ( 'NONE', #3936, #18559, #29641 ) ;
#33529=EDGE_CURVE ( 'NONE', #26918, #41311, #34083, .T. ) ;
#33530=CARTESIAN_POINT ( 'NONE',  ( 0.2559055118110208360, -0.01436877235161249967, -0.02740704184215201136 ) ) ;
#33558=ORIENTED_EDGE ( 'NONE', *, *, #20832, .T. ) ;
#33593=CARTESIAN_POINT ( 'NONE',  ( -0.2559055118110236116, 0.006260861050427609514, -0.3149606299212598381 ) ) ;
#33599=B_SPLINE_CURVE_WITH_KNOTS ( 'NONE', 3,
 ( #33741, #38479, #8530, #19555, #12631, #20024, #27256, #15986, #41808, #44695, #9007, #33968, #38242, #45173, #34664, #1095, #41562 ),
 .UNSPECIFIED., .F., .F.,
 ( 4, 2, 2, 2, 2, 1, 2, 2, 4 ),
 ( 0.000000000000000000, 0.1249999999999983902, 0.1874999999999975853, 0.2499999999999967804, 0.3749999999999956146, 0.4374999999999951150, 0.4687499999999949485, 0.4999999999999947820, 1.000000000000000000 ),
 .UNSPECIFIED. ) ;
#33615=ADVANCED_FACE ( 'NONE', ( #5715 ), #26188, .F. ) ;
#33617=DIRECTION ( 'NONE',  ( 0.4230299666438205319, 5.180622945937663512E-17, -0.9061156920180379881 ) ) ;
#33623=AXIS2_PLACEMENT_3D ( 'NONE', #37898, #23285, #44581 ) ;
#33625=ORIENTED_EDGE ( 'NONE', *, *, #27196, .T. ) ;
#33709=ORIENTED_EDGE ( 'NONE', *, *, #41235, .T. ) ;
#33717=DIRECTION ( 'NONE',  ( 0.000000000000000000, 0.000000000000000000, 1.000000000000000000 ) ) ;
#33732=DIRECTION ( 'NONE',  ( 0.000000000000000000, 0.000000000000000000, 1.000000000000000000 ) ) ;
#33741=CARTESIAN_POINT ( 'NONE',  ( -0.1279527559055118058, -0.2216206741968047289, -0.3149606299212598381 ) ) ;
#33750=ORIENTED_EDGE ( 'NONE', *, *, #33529, .F. ) ;
#33777=CONICAL_SURFACE ( 'NONE', #29990, 0.1574803149606299191, 0.9599310885968713736 ) ;
#33778=CARTESIAN_POINT ( 'NONE',  ( 0.2559046595376678335, -0.05435615997519514797, -0.03956173954060922260 ) ) ;
#33783=CIRCLE ( 'NONE', #28534, 0.1377952755905511861 ) ;
#33802=PLANE ( 'NONE',  #46713 ) ;
#33834=EDGE_CURVE ( 'NONE', #370, #40880, #27717, .T. ) ;
#33835=VECTOR ( 'NONE', #41202, 39.37007874015748143 ) ;
#33849=CARTESIAN_POINT ( 'NONE',  ( 0.009895589093209080853, 0.2897810112356523082, -0.09996720075266637973 ) ) ;
#33859=FACE_OUTER_BOUND ( 'NONE', #10298, .T. ) ;
#33900=EDGE_CURVE ( 'NONE', #1846, #3606, #7593, .T. ) ;
#33936=DIRECTION ( 'NONE',  ( 0.000000000000000000, 0.000000000000000000, 1.000000000000000000 ) ) ;
#33954=EDGE_CURVE ( 'NONE', #7920, #25562, #44239, .T. ) ;
#33968=CARTESIAN_POINT ( 'NONE',  ( -0.1872703683833633059, -0.1873733034530705444, -0.3097625555229961969 ) ) ;
#33972=FACE_OUTER_BOUND ( 'NONE', #23845, .T. ) ;
#34030=CARTESIAN_POINT ( 'NONE',  ( 0.2559055118110236116, -0.1477471161312047254, -0.1122047244094488277 ) ) ;
#34044=CARTESIAN_POINT ( 'NONE',  ( 0.000000000000000000, 0.000000000000000000, -0.3149606299212598381 ) ) ;
#34051=CARTESIAN_POINT ( 'NONE',  ( -0.04256392708709098860, -0.2709142457700946527, -0.3044102143378214498 ) ) ;
#34079=CARTESIAN_POINT ( 'NONE',  ( 0.1913749512857760571, 0.1850038654768927093, -0.3090319486758464906 ) ) ;
#34083=LINE ( 'NONE', #26655, #33835 ) ;
#34099=CONICAL_SURFACE ( 'NONE', #24876, 0.2559055118110236116, 1.047197551196597409 ) ;
#34113=CARTESIAN_POINT ( 'NONE',  ( -0.2559055118110236116, -0.06560852000721112409, -0.04485359485310594363 ) ) ;
#34114=EDGE_LOOP ( 'NONE', ( #31383, #33558, #41997, #21598 ) ) ;
#34126=CARTESIAN_POINT ( 'NONE',  ( -0.04257025887456828556, 0.2709160761542590556, -0.3049284531892009209 ) ) ;
#34158=ORIENTED_EDGE ( 'NONE', *, *, #31931, .T. ) ;
#34165=LINE ( 'NONE', #19516, #18828 ) ;
#34194=CARTESIAN_POINT ( 'NONE',  ( -0.1377952755905510751, 1.687505431895957647E-17, -0.3149606299212598381 ) ) ;
#34256=CARTESIAN_POINT ( 'NONE',  ( -0.1377952755905509363, 0.000000000000000000, -0.1045766232635885612 ) ) ;
#34286=CARTESIAN_POINT ( 'NONE',  ( 0.03734157890109738448, 0.2739282660277746473, -0.3031249188863235355 ) ) ;
#34288=AXIS2_PLACEMENT_3D ( 'NONE', #33216, #43242, #340 ) ;
#34299=EDGE_LOOP ( 'NONE', ( #33102, #38079, #32088, #9385 ) ) ;
#34319=EDGE_CURVE ( 'NONE', #41713, #45855, #23695, .T. ) ;
#34367=CARTESIAN_POINT ( 'NONE',  ( 0.2343326035694769383, -0.1601959449155855308, -0.2989494884450356049 ) ) ;
#34381=ORIENTED_EDGE ( 'NONE', *, *, #32539, .F. ) ;
#34388=CARTESIAN_POINT ( 'NONE',  ( 0.1711860128073784404, 0.1966586703794935831, -0.3122165016188708231 ) ) ;
#34480=LINE ( 'NONE', #23693, #44449 ) ;
#34481=CARTESIAN_POINT ( 'NONE',  ( 0.000000000000000000, 0.000000000000000000, -0.1183602362204724257 ) ) ;
#34518=EDGE_LOOP ( 'NONE', ( #27714, #29124, #31178, #29812 ) ) ;
#34519=ADVANCED_FACE ( 'NONE', ( #2805 ), #12437, .F. ) ;
#34536=VECTOR ( 'NONE', #18560, 39.37007874015748143 ) ;
#34561=LINE ( 'NONE', #20400, #14181 ) ;
#34565=CARTESIAN_POINT ( 'NONE',  ( -0.2559055118110236671, -0.04461241169208605278, -0.03567375012348084767 ) ) ;
#34599=CARTESIAN_POINT ( 'NONE',  ( 0.000000000000000000, 0.000000000000000000, -0.1966003937007873570 ) ) ;
#34616=ORIENTED_EDGE ( 'NONE', *, *, #41599, .T. ) ;
#34624=DIRECTION ( 'NONE',  ( 1.000000000000000000, 0.000000000000000000, 0.000000000000000000 ) ) ;
#34626=LINE ( 'NONE', #45610, #42271 ) ;
#34632=ORIENTED_EDGE ( 'NONE', *, *, #37493, .T. ) ;
#34643=ORIENTED_EDGE ( 'NONE', *, *, #37823, .F. ) ;
#34664=CARTESIAN_POINT ( 'NONE',  ( -0.2133350748062230740, -0.1723249637081083474, -0.3049284531890984473 ) ) ;
#34718=DIRECTION ( 'NONE',  ( 0.000000000000000000, 0.000000000000000000, 1.000000000000000000 ) ) ;
#34724=FACE_OUTER_BOUND ( 'NONE', #7966, .T. ) ;
#34733=CARTESIAN_POINT ( 'NONE',  ( 0.000000000000000000, 0.000000000000000000, -0.0004999999999998990712 ) ) ;
#34756=CARTESIAN_POINT ( 'NONE',  ( 0.1377952755905511861, 0.000000000000000000, -0.2103840066576717072 ) ) ;
#34776=AXIS2_PLACEMENT_3D ( 'NONE', #47203, #43830, #43591 ) ;
#34868=CARTESIAN_POINT ( 'NONE',  ( 0.1792139591738777793, 0.1920237930726759468, -0.3110703821948122005 ) ) ;
#34875=EDGE_CURVE ( 'NONE', #2629, #21809, #34626, .T. ) ;
#34878=EDGE_CURVE ( 'NONE', #873, #3606, #21617, .T. ) ;
#34891=AXIS2_PLACEMENT_3D ( 'NONE', #37086, #44261, #33292 ) ;
#34901=CARTESIAN_POINT ( 'NONE',  ( -0.1657445988168630702, 0.1998015435187649458, -0.03531881253560850004 ) ) ;
#34936=VERTEX_POINT ( 'NONE', #37739 ) ;
#34984=VERTEX_POINT ( 'NONE', #16182 ) ;
#35013=CARTESIAN_POINT ( 'NONE',  ( 0.1982027233128390575, 0.1810618366036217119, -0.05428606100831530334 ) ) ;
#35019=ADVANCED_FACE ( 'NONE', ( #35097 ), #40001, .F. ) ;
#35037=DIRECTION ( 'NONE',  ( 0.000000000000000000, 0.000000000000000000, 1.000000000000000000 ) ) ;
#35039=ORIENTED_EDGE ( 'NONE', *, *, #12090, .T. ) ;
#35040=DIRECTION ( 'NONE',  ( 0.000000000000000000, 0.000000000000000000, 1.000000000000000000 ) ) ;
#35045=ORIENTED_EDGE ( 'NONE', *, *, #7746, .F. ) ;
#35052=ORIENTED_EDGE ( 'NONE', *, *, #43050, .T. ) ;
#35097=FACE_OUTER_BOUND ( 'NONE', #2191, .T. ) ;
#35105=CARTESIAN_POINT ( 'NONE',  ( 0.1993772601175047565, -0.1803837174632775264, -0.05517042925146220522 ) ) ;
#35110=DIRECTION ( 'NONE',  ( 1.000000000000000000, 0.000000000000000000, 0.000000000000000000 ) ) ;
#35134=EDGE_CURVE ( 'NONE', #34936, #30980, #4870, .T. ) ;
#35144=ORIENTED_EDGE ( 'NONE', *, *, #15157, .T. ) ;
#35207=CARTESIAN_POINT ( 'NONE',  ( 0.1377952755905509363, 0.000000000000000000, -0.1436967020037460685 ) ) ;
#35224=CARTESIAN_POINT ( 'NONE',  ( 0.08476992594623591892, 0.2465534299916050109, -0.3121915932859317122 ) ) ;
#35248=DIRECTION ( 'NONE',  ( 1.000000000000000000, 0.000000000000000000, 0.000000000000000000 ) ) ;
#35254=CARTESIAN_POINT ( 'NONE',  ( 0.1849324350982721465, -0.1887234410765286363, -0.04495255068440705964 ) ) ;
#35256=CONICAL_SURFACE ( 'NONE', #8440, 0.1574803149606299191, 0.9599310885968735940 ) ;
#35261=CONICAL_SURFACE ( 'NONE', #1562, 0.2559055118110236116, 1.047197551196597409 ) ;
#35285=ORIENTED_EDGE ( 'NONE', *, *, #19482, .T. ) ;
#35315=ORIENTED_EDGE ( 'NONE', *, *, #33207, .T. ) ;
#35324=AXIS2_PLACEMENT_3D ( 'NONE', #41745, #1500, #27192 ) ;
#35352=VECTOR ( 'NONE', #26543, 39.37007874015748143 ) ;
#35362=CARTESIAN_POINT ( 'NONE',  ( -0.1667418150844807434, 0.1992258004382155001, -0.03573910814353464110 ) ) ;
#35414=DIRECTION ( 'NONE',  ( 1.000000000000000000, 0.000000000000000000, 0.000000000000000000 ) ) ;
#35424=AXIS2_PLACEMENT_3D ( 'NONE', #30040, #44583, #40288 ) ;
#35436=DIRECTION ( 'NONE',  ( -1.000000000000000000, 0.000000000000000000, 0.000000000000000000 ) ) ;
#35438=CIRCLE ( 'NONE', #20871, 0.1567662409572586624 ) ;
#35452=CARTESIAN_POINT ( 'NONE',  ( 0.06871726393438436220, 0.2558202476623961386, -0.3098131533094667933 ) ) ;
#35465=ADVANCED_FACE ( 'NONE', ( #5304 ), #36209, .F. ) ;
#35467=AXIS2_PLACEMENT_3D ( 'NONE', #29713, #44260, #3788 ) ;
#35484=CARTESIAN_POINT ( 'NONE',  ( 0.09631076833421682581, -0.2398891842387891882, -0.03294411891277762572 ) ) ;
#35486=CARTESIAN_POINT ( 'NONE',  ( 0.2559055118110236116, 0.1477471161312045311, -0.1122047244094488277 ) ) ;
#35508=DIRECTION ( 'NONE',  ( 0.000000000000000000, 0.000000000000000000, 1.000000000000000000 ) ) ;
#35511=DIRECTION ( 'NONE',  ( 1.000000000000000000, 0.000000000000000000, 0.000000000000000000 ) ) ;
#35537=EDGE_CURVE ( 'NONE', #38700, #23237, #41484, .T. ) ;
#35557=ORIENTED_EDGE ( 'NONE', *, *, #3461, .F. ) ;
#35570=ORIENTED_EDGE ( 'NONE', *, *, #46516, .T. ) ;
#35573=CARTESIAN_POINT ( 'NONE',  ( 0.2460099227178147996, -0.1534603371579595921, -0.09996720075266711525 ) ) ;
#35592=EDGE_CURVE ( 'NONE', #21809, #752, #182, .T. ) ;
#35614=ORIENTED_EDGE ( 'NONE', *, *, #41235, .F. ) ;
#35649=CARTESIAN_POINT ( 'NONE',  ( -0.2559055118110236116, 0.1477471161312031434, -0.1122047244094468571 ) ) ;
#35713=CARTESIAN_POINT ( 'NONE',  ( 0.06200172126963626046, -0.2596975217971643213, -0.05114647357132630356 ) ) ;
#35773=CARTESIAN_POINT ( 'NONE',  ( -0.2431102362204724532, 0.000000000000000000, 0.000000000000000000 ) ) ;
#35807=ORIENTED_EDGE ( 'NONE', *, *, #37823, .T. ) ;
#35819=CARTESIAN_POINT ( 'NONE',  ( -0.1017711380106712249, 0.2367366383362116133, -0.03112915705353517387 ) ) ;
#35857=DIRECTION ( 'NONE',  ( 0.000000000000000000, 0.000000000000000000, -1.000000000000000000 ) ) ;
#35863=ORIENTED_EDGE ( 'NONE', *, *, #998, .F. ) ;
#35887=DIRECTION ( 'NONE',  ( -0.8191520442889861364, 1.003171929053517844E-16, 0.5735764363510541530 ) ) ;
#35928=( CONVERSION_BASED_UNIT ( 'INCH', #20836 ) LENGTH_UNIT ( ) NAMED_UNIT ( #17625 ) ) ;
#35976=EDGE_CURVE ( 'NONE', #9930, #18657, #24168, .T. ) ;
#35977=DIRECTION ( 'NONE',  ( 1.000000000000000000, 0.000000000000000000, 0.000000000000000000 ) ) ;
#36070=ORIENTED_EDGE ( 'NONE', *, *, #10741, .F. ) ;
#36083=CARTESIAN_POINT ( 'NONE',  ( -0.1377952755905513527, 1.687505431895961344E-17, -0.3001770169643759867 ) ) ;
#36106=VECTOR ( 'NONE', #11833, 39.37007874015748854 ) ;
#36125=CARTESIAN_POINT ( 'NONE',  ( -0.2559055118110236116, 0.08129156908512058521, -0.05439871778755192566 ) ) ;
#36126=CONICAL_SURFACE ( 'NONE', #5511, 0.2559055118110236116, 1.047197551196597409 ) ;
#36144=CARTESIAN_POINT ( 'NONE',  ( 0.2559055118110236116, 0.1477471161312027548, -0.3149606299212598381 ) ) ;
#36182=CARTESIAN_POINT ( 'NONE',  ( -0.1377952755905511861, 1.808041534174241898E-17, -0.2495040853978291451 ) ) ;
#36193=CARTESIAN_POINT ( 'NONE',  ( 0.07691592068038602403, -0.2510868047526202962, -0.04147023971060104924 ) ) ;
#36209=CONICAL_SURFACE ( 'NONE', #30854, 0.1574803149606299191, 0.9599310885968735940 ) ;
#36260=ORIENTED_EDGE ( 'NONE', *, *, #16477, .F. ) ;
#36273=DIRECTION ( 'NONE',  ( -0.8191520442889873577, 1.003171929053519323E-16, 0.5735764363510523767 ) ) ;
#36370=CARTESIAN_POINT ( 'NONE',  ( 0.06594017991656314637, -0.2574235754679920496, -0.3092881115733853714 ) ) ;
#36379=DIRECTION ( 'NONE',  ( 0.000000000000000000, 0.000000000000000000, 1.000000000000000000 ) ) ;
#36448=ORIENTED_EDGE ( 'NONE', *, *, #35592, .T. ) ;
#36473=LENGTH_MEASURE_WITH_UNIT ( LENGTH_MEASURE( 0.02539999999999999897 ), #40032 ) ;
#36484=ADVANCED_FACE ( 'NONE', ( #17545 ), #5529, .T. ) ;
#36490=CARTESIAN_POINT ( 'NONE',  ( -0.2559055118110236116, -4.908314874579054539E-16, -0.02740704184215039460 ) ) ;
#36508=CARTESIAN_POINT ( 'NONE',  ( -0.1623289600446945202, -0.2017735634833314473, -0.03395687952546246058 ) ) ;
#36530=AXIS2_PLACEMENT_3D ( 'NONE', #44768, #8598, #30448 ) ;
#36538=CARTESIAN_POINT ( 'NONE',  ( -0.01990234270466676239, 0.2840036093443637499, -0.08759220388352539910 ) ) ;
#36543=CARTESIAN_POINT ( 'NONE',  ( 0.1377952755905510751, 1.687505431895957647E-17, -0.02633646578327370619 ) ) ;
#36566=DIRECTION ( 'NONE',  ( 1.000000000000000000, 0.000000000000000000, 0.000000000000000000 ) ) ;
#36573=CARTESIAN_POINT ( 'NONE',  ( -0.2559055118110235560, -0.04862481504115584441, -0.03719749321262351416 ) ) ;
#36586=EDGE_CURVE ( 'NONE', #34984, #14850, #4557, .T. ) ;
#36595=FACE_OUTER_BOUND ( 'NONE', #20177, .T. ) ;
#36601=CARTESIAN_POINT ( 'NONE',  ( 0.000000000000000000, 0.000000000000000000, 0.000000000000000000 ) ) ;
#36605=FACE_OUTER_BOUND ( 'NONE', #27639, .T. ) ;
#36651=DIRECTION ( 'NONE',  ( 1.000000000000000000, 0.000000000000000000, 0.000000000000000000 ) ) ;
#36698=DIRECTION ( 'NONE',  ( 0.000000000000000000, 0.000000000000000000, 1.000000000000000000 ) ) ;
#36708=CARTESIAN_POINT ( 'NONE',  ( 0.1377952755905510474, 1.687505431895957647E-17, -0.2610569382242185488 ) ) ;
#36714=ORIENTED_EDGE ( 'NONE', *, *, #29963, .T. ) ;
#36719=ADVANCED_FACE ( 'NONE', ( #38355 ), #36126, .T. ) ;
#36733=CARTESIAN_POINT ( 'NONE',  ( -0.05614424849857162919, -0.2630793352783083461, -0.05546260682012697785 ) ) ;
#36753=ORIENTED_EDGE ( 'NONE', *, *, #33083, .T. ) ;
#36806=ORIENTED_EDGE ( 'NONE', *, *, #34319, .T. ) ;
#36807=CARTESIAN_POINT ( 'NONE',  ( -0.2559055118110235560, -0.07545482141442715063, -0.05057764367740170269 ) ) ;
#36820=AXIS2_PLACEMENT_3D ( 'NONE', #8589, #24399, #27321 ) ;
#36829=CARTESIAN_POINT ( 'NONE',  ( 0.04257025887484965077, -0.2709160761539660123, -0.3049284531893265981 ) ) ;
#36836=DIRECTION ( 'NONE',  ( 1.000000000000000000, 0.000000000000000000, 0.000000000000000000 ) ) ;
#36866=CARTESIAN_POINT ( 'NONE',  ( 0.2559055015491151774, -0.08324699190379426794, -0.05567992556649694474 ) ) ;
#36881=DIRECTION ( 'NONE',  ( 0.8191520442889873577, 0.000000000000000000, 0.5735764363510523767 ) ) ;
#36885=ORIENTED_EDGE ( 'NONE', *, *, #33954, .F. ) ;
#36959=EDGE_LOOP ( 'NONE', ( #997, #13110, #47044, #7860 ) ) ;
#36975=ORIENTED_EDGE ( 'NONE', *, *, #3757, .F. ) ;
#36989=CYLINDRICAL_SURFACE ( 'NONE', #10380, 0.1377952755905511029 ) ;
#37002=DIRECTION ( 'NONE',  ( 0.000000000000000000, 0.000000000000000000, -1.000000000000000000 ) ) ;
#37069=EDGE_CURVE ( 'NONE', #9873, #16859, #3540, .T. ) ;
#37085=CARTESIAN_POINT ( 'NONE',  ( 0.000000000000000000, 0.000000000000000000, 2.731847993664263218E-16 ) ) ;
#37086=CARTESIAN_POINT ( 'NONE',  ( 0.000000000000000000, 0.000000000000000000, -0.2610569382242185488 ) ) ;
#37092=CARTESIAN_POINT ( 'NONE',  ( 0.2559054078461202586, -0.02857456808055104658, -0.02996975140571832980 ) ) ;
#37094=ORIENTED_EDGE ( 'NONE', *, *, #34319, .F. ) ;
#37232=CARTESIAN_POINT ( 'NONE',  ( 0.000000000000000000, 0.000000000000000000, -0.04012007874015743186 ) ) ;
#37278=CARTESIAN_POINT ( 'NONE',  ( 0.07267052687100558628, -0.2535370473714794182, -0.3104511204119563272 ) ) ;
#37321=CIRCLE ( 'NONE', #23597, 0.1377952755905511861 ) ;
#37328=ORIENTED_EDGE ( 'NONE', *, *, #46234, .T. ) ;
#37345=VECTOR ( 'NONE', #15324, 39.37007874015748143 ) ;
#37378=EDGE_CURVE ( 'NONE', #2629, #16719, #27874, .T. ) ;
#37396=CARTESIAN_POINT ( 'NONE',  ( 0.1872703683832034893, 0.1873733034532325537, -0.3097625555229955863 ) ) ;
#37432=ORIENTED_EDGE ( 'NONE', *, *, #16413, .T. ) ;
#37433=AXIS2_PLACEMENT_3D ( 'NONE', #6562, #42022, #16658 ) ;
#37454=LINE ( 'NONE', #772, #19256 ) ;
#37456=CARTESIAN_POINT ( 'NONE',  ( 0.000000000000000000, 0.000000000000000000, -0.3149606299212598381 ) ) ;
#37475=ORIENTED_EDGE ( 'NONE', *, *, #8326, .F. ) ;
#37485=ORIENTED_EDGE ( 'NONE', *, *, #27094, .T. ) ;
#37488=ORIENTED_EDGE ( 'NONE', *, *, #17257, .T. ) ;
#37493=EDGE_CURVE ( 'NONE', #18657, #16796, #46988, .T. ) ;
#37517=DIRECTION ( 'NONE',  ( 0.000000000000000000, 0.000000000000000000, 1.000000000000000000 ) ) ;
#37549=CARTESIAN_POINT ( 'NONE',  ( 3.127876812047771422E-16, 0.2954942322624074524, -0.3149606299212598381 ) ) ;
#37607=EDGE_CURVE ( 'NONE', #31834, #9930, #13355, .T. ) ;
#37613=CARTESIAN_POINT ( 'NONE',  ( -0.09272654090491234957, -0.2419614285902609574, -0.3131151337379051713 ) ) ;
#37632=AXIS2_PLACEMENT_3D ( 'NONE', #17912, #39234, #21022 ) ;
#37684=CARTESIAN_POINT ( 'NONE',  ( -0.2559055118110235560, -0.04381123493339342950, -0.03538144886923444421 ) ) ;
#37695=CARTESIAN_POINT ( 'NONE',  ( -0.1171060910373939445, 0.2278812977176828125, -0.3148284977848753718 ) ) ;
#37700=CONICAL_SURFACE ( 'NONE', #30861, 0.1574803149606299191, 0.9599310885968735940 ) ;
#37717=LINE ( 'NONE', #4868, #23746 ) ;
#37726=CARTESIAN_POINT ( 'NONE',  ( 0.1377952755905510751, 0.000000000000000000, -0.3149606299212598381 ) ) ;
#37737=DIRECTION ( 'NONE',  ( 0.000000000000000000, 0.000000000000000000, 1.000000000000000000 ) ) ;
#37738=DIRECTION ( 'NONE',  ( 0.000000000000000000, 0.000000000000000000, 1.000000000000000000 ) ) ;
#37739=CARTESIAN_POINT ( 'NONE',  ( -2.458663194297838277E-15, -0.2954942322624074524, -0.1122047244094488277 ) ) ;
#37786=CARTESIAN_POINT ( 'NONE',  ( -0.1377952755905513804, 0.000000000000000000, -0.3001770169643759867 ) ) ;
#37823=EDGE_CURVE ( 'NONE', #752, #21809, #17198, .T. ) ;
#37898=CARTESIAN_POINT ( 'NONE',  ( 0.000000000000000000, 0.000000000000000000, -0.0009999999999999347518 ) ) ;
#37919=PLANE ( 'NONE',  #2265 ) ;
#37924=CARTESIAN_POINT ( 'NONE',  ( -0.2559055118110236116, -4.908314874579054539E-16, -0.02740704184215039460 ) ) ;
#37960=CARTESIAN_POINT ( 'NONE',  ( 0.2559055118110236116, -0.1477471161312049197, -0.2921040715117803055 ) ) ;
#37967=EDGE_LOOP ( 'NONE', ( #43479, #7490, #46158 ) ) ;
#37975=CARTESIAN_POINT ( 'NONE',  ( 0.1658511544268519433, 0.1997399692764126045, -0.3128573757128086941 ) ) ;
#38038=CARTESIAN_POINT ( 'NONE',  ( -0.2016454051084722587, 0.1790725142611516163, -0.3070225280280141633 ) ) ;
#38057=DIRECTION ( 'NONE',  ( 1.000000000000000000, 0.000000000000000000, 0.000000000000000000 ) ) ;
#38076=DIRECTION ( 'NONE',  ( 0.000000000000000000, 0.000000000000000000, -1.000000000000000000 ) ) ;
#38079=ORIENTED_EDGE ( 'NONE', *, *, #17149, .T. ) ;
#38081=FACE_OUTER_BOUND ( 'NONE', #27387, .T. ) ;
#38176=DIRECTION ( 'NONE',  ( 0.000000000000000000, 0.000000000000000000, 1.000000000000000000 ) ) ;
#38191=DIRECTION ( 'NONE',  ( 1.000000000000000000, 0.000000000000000000, 0.000000000000000000 ) ) ;
#38226=CARTESIAN_POINT ( 'NONE',  ( -0.2559082475277629221, -0.04046285581729015118, -0.3131342661657301463 ) ) ;
#38242=CARTESIAN_POINT ( 'NONE',  ( -0.1899652659300057611, -0.1858176586718346124, -0.3092881115734000819 ) ) ;
#38270=ORIENTED_EDGE ( 'NONE', *, *, #42984, .F. ) ;
#38281=DIRECTION ( 'NONE',  ( 1.000000000000000000, 0.000000000000000000, 0.000000000000000000 ) ) ;
#38285=CARTESIAN_POINT ( 'NONE',  ( 0.000000000000000000, 0.000000000000000000, -0.1183602362204724257 ) ) ;
#38303=CARTESIAN_POINT ( 'NONE',  ( -0.2559055118110236116, 0.1477471161312047254, -0.2921040715117803055 ) ) ;
#38304=DIRECTION ( 'NONE',  ( -0.8191520442889991260, 0.000000000000000000, -0.5735764363510355013 ) ) ;
#38307=ADVANCED_FACE ( 'NONE', ( #17918 ), #25365, .F. ) ;
#38310=ORIENTED_EDGE ( 'NONE', *, *, #10738, .T. ) ;
#38328=VECTOR ( 'NONE', #3887, 39.37007874015748143 ) ;
#38348=CIRCLE ( 'NONE', #21518, 0.1574803149606299191 ) ;
#38355=FACE_OUTER_BOUND ( 'NONE', #40315, .T. ) ;
#38361=CYLINDRICAL_SURFACE ( 'NONE', #15558, 0.1377952755905510751 ) ;
#38388=VECTOR ( 'NONE', #21745, 39.37007874015748143 ) ;
#38463=CARTESIAN_POINT ( 'NONE',  ( -0.2559055118110235560, -0.01245242171185129317, -0.3149606299212599492 ) ) ;
#38479=CARTESIAN_POINT ( 'NONE',  ( -0.1333875707376347142, -0.2184828823904832185, -0.3149606299212598381 ) ) ;
#38506=VERTEX_POINT ( 'NONE', #10758 ) ;
#38510=CARTESIAN_POINT ( 'NONE',  ( -0.1951724573785008632, 0.1828112239219657764, -0.3083162604245049954 ) ) ;
#38546=DIRECTION ( 'NONE',  ( 0.000000000000000000, 0.000000000000000000, 1.000000000000000000 ) ) ;
#38561=B_SPLINE_CURVE_WITH_KNOTS ( 'NONE', 3,
 ( #9659, #13948, #13485, #21366, #46293, #6510, #31471, #46054, #46528, #28115, #5819, #17539 ),
 .UNSPECIFIED., .F., .F.,
 ( 4, 1, 1, 1, 1, 2, 2, 4 ),
 ( 0.000000000000000000, 0.2500000000000012768, 0.3750000000000018874, 0.4375000000000021094, 0.4687500000000022204, 0.4843750000000023870, 0.5000000000000022204, 1.000000000000000000 ),
 .UNSPECIFIED. ) ;
#38599=CARTESIAN_POINT ( 'NONE',  ( 0.000000000000000000, 0.000000000000000000, -0.3149606299212598381 ) ) ;
#38605=DIRECTION ( 'NONE',  ( 1.000000000000000000, 0.000000000000000000, 0.000000000000000000 ) ) ;
#38615=ORIENTED_EDGE ( 'NONE', *, *, #28615, .F. ) ;
#38617=AXIS2_PLACEMENT_3D ( 'NONE', #45928, #27777, #13140 ) ;
#38637=CARTESIAN_POINT ( 'NONE',  ( -0.08471839801768285549, 0.2465807710546494280, -0.3122165016185723951 ) ) ;
#38645=DIRECTION ( 'NONE',  ( 0.8191520442889873577, 0.000000000000000000, 0.5735764363510523767 ) ) ;
#38672=CARTESIAN_POINT ( 'NONE',  ( 0.000000000000000000, 0.000000000000000000, -0.07924015748031493223 ) ) ;
#38675=ORIENTED_EDGE ( 'NONE', *, *, #29563, .T. ) ;
#38700=VERTEX_POINT ( 'NONE', #16002 ) ;
#38714=CARTESIAN_POINT ( 'NONE',  ( -0.2071276943281862848, 0.1759090021854023134, -0.06129781628412492994 ) ) ;
#38751=DIRECTION ( 'NONE',  ( 1.000000000000000000, 0.000000000000000000, 0.000000000000000000 ) ) ;
#38761=DIRECTION ( 'NONE',  ( 1.000000000000000000, 0.000000000000000000, 0.000000000000000000 ) ) ;
#38762=ORIENTED_EDGE ( 'NONE', *, *, #6215, .T. ) ;
#38809=CARTESIAN_POINT ( 'NONE',  ( 0.2559029816877552155, 0.01435274667127873181, -0.02805003521115247145 ) ) ;
#38814=AXIS2_PLACEMENT_3D ( 'NONE', #27810, #46909, #16749 ) ;
#38825=CARTESIAN_POINT ( 'NONE',  ( -2.458663194297838277E-15, -0.2954942322624074524, -0.1122047244094488277 ) ) ;
#38857=VECTOR ( 'NONE', #5108, 39.37007874015748143 ) ;
#38861=VERTEX_POINT ( 'NONE', #31797 ) ;
#38867=DIRECTION ( 'NONE',  ( -0.000000000000000000, -0.000000000000000000, -1.000000000000000000 ) ) ;
#38881=CARTESIAN_POINT ( 'NONE',  ( 0.2559055118110236116, 0.1477471161312045311, -0.2921040715117803055 ) ) ;
#38888=CARTESIAN_POINT ( 'NONE',  ( 0.1977610074737742307, -0.1813162243849978650, -0.3078067560680141090 ) ) ;
#38895=AXIS2_PLACEMENT_3D ( 'NONE', #27556, #45707, #41869 ) ;
#38915=CARTESIAN_POINT ( 'NONE',  ( 0.1574803149606299191, 0.000000000000000000, -0.07924015748031493223 ) ) ;
#38922=CARTESIAN_POINT ( 'NONE',  ( -0.2559066715754571564, -0.04966882545208399502, -0.3122129920274815951 ) ) ;
#38957=CIRCLE ( 'NONE', #20593, 0.1377952755905511861 ) ;
#38972=CONICAL_SURFACE ( 'NONE', #20606, 0.1574803149606299191, 0.9599310885968735940 ) ;
#39032=LINE ( 'NONE', #6440, #21835 ) ;
#39051=CARTESIAN_POINT ( 'NONE',  ( 0.1642836037694651863, 0.2006450494026638109, -0.03472289316813669674 ) ) ;
#39071=DIRECTION ( 'NONE',  ( 0.000000000000000000, 0.000000000000000000, 1.000000000000000000 ) ) ;
#39108=DIRECTION ( 'NONE',  ( 0.000000000000000000, 0.000000000000000000, 1.000000000000000000 ) ) ;
#39122=ADVANCED_FACE ( 'NONE', ( #33227 ), #13475, .F. ) ;
#39144=DIRECTION ( 'NONE',  ( 0.000000000000000000, 0.000000000000000000, 1.000000000000000000 ) ) ;
#39152=EDGE_CURVE ( 'NONE', #16719, #2, #34165, .T. ) ;
#39161=DIRECTION ( 'NONE',  ( 0.000000000000000000, 0.000000000000000000, 1.000000000000000000 ) ) ;
#39165=CARTESIAN_POINT ( 'NONE',  ( 0.1574803149606299191, 1.928577636452524918E-17, -0.2357204724409448504 ) ) ;
#39194=CIRCLE ( 'NONE', #18541, 0.1377952755905511861 ) ;
#39199=CARTESIAN_POINT ( 'NONE',  ( 0.000000000000000000, 0.000000000000000000, -0.3149606299212598381 ) ) ;
#39201=ORIENTED_EDGE ( 'NONE', *, *, #11110, .T. ) ;
#39230=CARTESIAN_POINT ( 'NONE',  ( 0.000000000000000000, 0.000000000000000000, -0.1966003937007873570 ) ) ;
#39234=DIRECTION ( 'NONE',  ( 0.000000000000000000, 0.000000000000000000, 1.000000000000000000 ) ) ;
#39250=ORIENTED_EDGE ( 'NONE', *, *, #46150, .T. ) ;
#39265=VECTOR ( 'NONE', #9133, 39.37007874015748143 ) ;
#39283=CARTESIAN_POINT ( 'NONE',  ( 0.1126596235262874585, -0.2304501682927049544, -0.02834147079956455748 ) ) ;
#39285=CARTESIAN_POINT ( 'NONE',  ( 0.1939037905413676932, 0.1835438265964589033, -0.05114647357130735345 ) ) ;
#39341=CARTESIAN_POINT ( 'NONE',  ( 0.2559055118110236671, 0.03078476920768365155, -0.3141842412145660068 ) ) ;
#39346=CARTESIAN_POINT ( 'NONE',  ( 0.000000000000000000, 0.000000000000000000, -0.09302377043719921301 ) ) ;
#39349=EDGE_CURVE ( 'NONE', #43008, #42075, #31774, .T. ) ;
#39379=ORIENTED_EDGE ( 'NONE', *, *, #27367, .T. ) ;
#39390=CARTESIAN_POINT ( 'NONE',  ( -0.1404189863467107946, 0.2144232926957992391, -0.02742975588280811491 ) ) ;
#39434=AXIS2_PLACEMENT_3D ( 'NONE', #19049, #33717, #12125 ) ;
#39438=DIRECTION ( 'NONE',  ( 0.5000000000000003331, -0.8660254037844384856, 0.000000000000000000 ) ) ;
#39444=CYLINDRICAL_SURFACE ( 'NONE', #16473, 0.1377952755905511029 ) ;
#39463=CARTESIAN_POINT ( 'NONE',  ( -0.2559055118110236116, 0.07922414731028902535, -0.05306965205172459177 ) ) ;
#39497=CARTESIAN_POINT ( 'NONE',  ( 0.2559046883225459812, 0.07066125644906998127, -0.04784811367750762406 ) ) ;
#39511=DIRECTION ( 'NONE',  ( 0.000000000000000000, 0.000000000000000000, 1.000000000000000000 ) ) ;
#39519=CARTESIAN_POINT ( 'NONE',  ( 0.06699593397070344181, -0.2568141117498130566, -0.04769437235513194345 ) ) ;
#39536=ORIENTED_EDGE ( 'NONE', *, *, #12090, .F. ) ;
#39541=EDGE_LOOP ( 'NONE', ( #27146, #12945, #14336, #21413 ) ) ;
#39570=LINE ( 'NONE', #24734, #14251 ) ;
#39579=FACE_OUTER_BOUND ( 'NONE', #9131, .T. ) ;
#39686=CARTESIAN_POINT ( 'NONE',  ( -0.2559055118110235005, 0.03992503320406630418, -0.03403288757427296030 ) ) ;
#39695=CARTESIAN_POINT ( 'NONE',  ( 0.1279527559055118058, -0.2216206741968047289, -0.3149606299212598381 ) ) ;
#39720=CARTESIAN_POINT ( 'NONE',  ( 0.2559049618366861512, 0.03677276663233821491, -0.03301314027812483204 ) ) ;
#39728=ORIENTED_EDGE ( 'NONE', *, *, #33032, .F. ) ;
#39735=( LENGTH_UNIT ( ) NAMED_UNIT ( * ) SI_UNIT ( $, .METRE. ) ) ;
#39744=DIRECTION ( 'NONE',  ( 0.000000000000000000, 0.000000000000000000, 1.000000000000000000 ) ) ;
#39783=VERTEX_POINT ( 'NONE', #40511 ) ;
#39786=DIRECTION ( 'NONE',  ( 1.000000000000000000, 0.000000000000000000, 0.000000000000000000 ) ) ;
#39791=CARTESIAN_POINT ( 'NONE',  ( 0.000000000000000000, 0.000000000000000000, -0.2610569382242185488 ) ) ;
#39810=CARTESIAN_POINT ( 'NONE',  ( 0.2559055118110236116, 0.07425961573522271708, -0.3088661881183391578 ) ) ;
#39831=CARTESIAN_POINT ( 'NONE',  ( -0.1642836037694702656, -0.2006450494026624509, -0.03472289316814061721 ) ) ;
#39839=VECTOR ( 'NONE', #30613, 39.37007874015748143 ) ;
#39850=ORIENTED_EDGE ( 'NONE', *, *, #35976, .F. ) ;
#39854=FACE_OUTER_BOUND ( 'NONE', #24256, .T. ) ;
#39865=LINE ( 'NONE', #7054, #46233 ) ;
#39928=CARTESIAN_POINT ( 'NONE',  ( 0.000000000000000000, 0.000000000000000000, -0.3149606299212598381 ) ) ;
#39933=CARTESIAN_POINT ( 'NONE',  ( -0.2559055118110235560, 0.08195668352890772557, -0.05483160856164565750 ) ) ;
#39937=DIRECTION ( 'NONE',  ( 0.000000000000000000, 0.000000000000000000, 1.000000000000000000 ) ) ;
#39940=LINE ( 'NONE', #6645, #40680 ) ;
#40001=CONICAL_SURFACE ( 'NONE', #18574, 0.1574803149606299191, 0.9599310885968735940 ) ;
#40024=VERTEX_POINT ( 'NONE', #32556 ) ;
#40026=ORIENTED_EDGE ( 'NONE', *, *, #37378, .T. ) ;
#40027=ORIENTED_EDGE ( 'NONE', *, *, #37607, .T. ) ;
#40032=( LENGTH_UNIT ( ) NAMED_UNIT ( * ) SI_UNIT ( $, .METRE. ) ) ;
#40045=CARTESIAN_POINT ( 'NONE',  ( -0.1377952755905509641, 1.687505431895957030E-17, -0.06545654452343109553 ) ) ;
#40091=LINE ( 'NONE', #46581, #24945 ) ;
#40140=AXIS2_PLACEMENT_3D ( 'NONE', #18237, #43384, #22064 ) ;
#40149=VERTEX_POINT ( 'NONE', #17136 ) ;
#40163=DIRECTION ( 'NONE',  ( -1.000000000000000000, 0.000000000000000000, 0.000000000000000000 ) ) ;
#40166=CARTESIAN_POINT ( 'NONE',  ( 0.000000000000000000, 0.000000000000000000, -0.1321438491773566926 ) ) ;
#40206=ORIENTED_EDGE ( 'NONE', *, *, #29050, .T. ) ;
#40216=EDGE_LOOP ( 'NONE', ( #41407, #4348, #35315, #45803 ) ) ;
#40225=EDGE_LOOP ( 'NONE', ( #41117, #42009, #23735, #6072 ) ) ;
#40267=EDGE_LOOP ( 'NONE', ( #31054, #45878, #40414, #44677, #21241, #30960 ) ) ;
#40269=( NAMED_UNIT ( * ) SI_UNIT ( $, .STERADIAN. ) SOLID_ANGLE_UNIT ( ) ) ;
#40288=DIRECTION ( 'NONE',  ( -1.000000000000000000, 0.000000000000000000, 0.000000000000000000 ) ) ;
#40303=CARTESIAN_POINT ( 'NONE',  ( -0.08916369672655032053, -0.2440155479553919315, -0.03573910814353623705 ) ) ;
#40315=EDGE_LOOP ( 'NONE', ( #13126, #25063, #35052 ) ) ;
#40323=CARTESIAN_POINT ( 'NONE',  ( -0.1377952755905510751, 1.687505431895957647E-17, -0.3149606299212598381 ) ) ;
#40384=ADVANCED_FACE ( 'NONE', ( #44175 ), #20489, .F. ) ;
#40412=CIRCLE ( 'NONE', #47313, 0.1377952755905511861 ) ;
#40414=ORIENTED_EDGE ( 'NONE', *, *, #18590, .T. ) ;
#40453=ADVANCED_FACE ( 'NONE', ( #26238 ), #43438, .T. ) ;
#40495=ORIENTED_EDGE ( 'NONE', *, *, #16669, .T. ) ;
#40511=CARTESIAN_POINT ( 'NONE',  ( -0.1377952755905511861, 1.808041534174241898E-17, -0.05390369169704170571 ) ) ;
#40532=CARTESIAN_POINT ( 'NONE',  ( -0.05275478416827693307, -0.2650362434218126451, -0.05809220732313855745 ) ) ;
#40607=ORIENTED_EDGE ( 'NONE', *, *, #16723, .F. ) ;
#40641=ORIENTED_EDGE ( 'NONE', *, *, #17864, .T. ) ;
#40662=CARTESIAN_POINT ( 'NONE',  ( 0.2559055118110236116, -0.1477471161312047254, -0.1122047244094488277 ) ) ;
#40680=VECTOR ( 'NONE', #35887, 39.37007874015748143 ) ;
#40693=CARTESIAN_POINT ( 'NONE',  ( 2.219626494852212756E-16, 0.2954942322624074524, -0.1122047244094488277 ) ) ;
#40705=CARTESIAN_POINT ( 'NONE',  ( -0.06871726393444720082, -0.2558202476623576138, -0.3098131533094798384 ) ) ;
#40711=EDGE_CURVE ( 'NONE', #1339, #4869, #45359, .T. ) ;
#40765=CARTESIAN_POINT ( 'NONE',  ( -0.09016091299416130467, -0.2434398048748465382, -0.03531881253561287154 ) ) ;
#40777=EDGE_CURVE ( 'NONE', #39783, #28164, #31023, .T. ) ;
#40803=DIRECTION ( 'NONE',  ( -1.000000000000000000, 0.000000000000000000, 0.000000000000000000 ) ) ;
#40829=CARTESIAN_POINT ( 'NONE',  ( 0.000000000000000000, 0.000000000000000000, -0.2748405511811023438 ) ) ;
#40880=VERTEX_POINT ( 'NONE', #28852 ) ;
#40898=CARTESIAN_POINT ( 'NONE',  ( 0.2559055126074655240, -0.08240829719531699016, -0.05512736142437904552 ) ) ;
#40926=ORIENTED_EDGE ( 'NONE', *, *, #35537, .T. ) ;
#40996=LINE ( 'NONE', #33165, #38328 ) ;
#41011=DIRECTION ( 'NONE',  ( 0.000000000000000000, 0.000000000000000000, 1.000000000000000000 ) ) ;
#41032=DIRECTION ( 'NONE',  ( 0.000000000000000000, 0.000000000000000000, 1.000000000000000000 ) ) ;
#41117=ORIENTED_EDGE ( 'NONE', *, *, #10738, .F. ) ;
#41136=ORIENTED_EDGE ( 'NONE', *, *, #15157, .F. ) ;
#41202=DIRECTION ( 'NONE',  ( 0.000000000000000000, 0.000000000000000000, 1.000000000000000000 ) ) ;
#41226=DIRECTION ( 'NONE',  ( 1.000000000000000000, 0.000000000000000000, 0.000000000000000000 ) ) ;
#41235=EDGE_CURVE ( 'NONE', #31435, #39783, #27007, .T. ) ;
#41273=CARTESIAN_POINT ( 'NONE',  ( 0.000000000000000000, 0.000000000000000000, -0.0004999999999998990712 ) ) ;
#41311=VERTEX_POINT ( 'NONE', #1085 ) ;
#41365=CARTESIAN_POINT ( 'NONE',  ( 0.2559055108844309201, -0.04382127000173715453, -0.03538492399873669619 ) ) ;
#41369=CARTESIAN_POINT ( 'NONE',  ( 0.1377952755905511029, 0.000000000000000000, -0.3149606299212598381 ) ) ;
#41380=DIRECTION ( 'NONE',  ( 0.000000000000000000, 0.000000000000000000, 1.000000000000000000 ) ) ;
#41388=AXIS2_PLACEMENT_3D ( 'NONE', #34599, #1750, #9433 ) ;
#41389=FACE_OUTER_BOUND ( 'NONE', #11194, .T. ) ;
#41393=DIRECTION ( 'NONE',  ( 1.000000000000000000, 0.000000000000000000, 0.000000000000000000 ) ) ;
#41407=ORIENTED_EDGE ( 'NONE', *, *, #36586, .F. ) ;
#41416=CARTESIAN_POINT ( 'NONE',  ( 0.02156745609636135860, 0.2830359600832316747, -0.2989494884453828272 ) ) ;
#41421=DIRECTION ( 'NONE',  ( 1.000000000000000000, 0.000000000000000000, 0.000000000000000000 ) ) ;
#41434=EDGE_LOOP ( 'NONE', ( #26751, #15835, #14418, #20776 ) ) ;
#41435=CONICAL_SURFACE ( 'NONE', #16977, 0.1574803149606299191, 0.9599310885968735940 ) ;
#41484=CIRCLE ( 'NONE', #22402, 0.1574803149606299191 ) ;
#41513=DIRECTION ( 'NONE',  ( 0.000000000000000000, 0.000000000000000000, 1.000000000000000000 ) ) ;
#41545=ORIENTED_EDGE ( 'NONE', *, *, #28623, .F. ) ;
#41562=CARTESIAN_POINT ( 'NONE',  ( -0.2559055118110236116, -0.1477471161312047254, -0.2921040715117803055 ) ) ;
#41573=CONICAL_SURFACE ( 'NONE', #13305, 0.2431102362204724532, 0.4367866272367255109 ) ;
#41576=DIRECTION ( 'NONE',  ( 0.000000000000000000, 0.000000000000000000, 1.000000000000000000 ) ) ;
#41580=CARTESIAN_POINT ( 'NONE',  ( 0.000000000000000000, 0.000000000000000000, -0.1574803149606298636 ) ) ;
#41599=EDGE_CURVE ( 'NONE', #40880, #370, #4157, .T. ) ;
#41600=CARTESIAN_POINT ( 'NONE',  ( 0.2559023402149968041, -0.1254131385238003160, -0.08931362558432201504 ) ) ;
#41607=ADVANCED_FACE ( 'NONE', ( #30759 ), #23071, .F. ) ;
#41627=DIRECTION ( 'NONE',  ( 0.000000000000000000, 0.000000000000000000, 1.000000000000000000 ) ) ;
#41652=ORIENTED_EDGE ( 'NONE', *, *, #10658, .F. ) ;
#41656=CARTESIAN_POINT ( 'NONE',  ( 0.05425864391567861156, 0.2641663005107173223, -0.3070225280281027036 ) ) ;
#41667=AXIS2_PLACEMENT_3D ( 'NONE', #17494, #15934, #45367 ) ;
#41670=CIRCLE ( 'NONE', #40140, 0.1377952755905511861 ) ;
#41672=CONICAL_SURFACE ( 'NONE', #21025, 0.1567662409572586624, 0.9599310885969887241 ) ;
#41713=VERTEX_POINT ( 'NONE', #20167 ) ;
#41717=VERTEX_POINT ( 'NONE', #24021 ) ;
#41719=EDGE_CURVE ( 'NONE', #31435, #15186, #24717, .T. ) ;
#41726=ORIENTED_EDGE ( 'NONE', *, *, #7734, .F. ) ;
#41738=CARTESIAN_POINT ( 'NONE',  ( 0.000000000000000000, 0.000000000000000000, -0.0004999999999998990712 ) ) ;
#41745=CARTESIAN_POINT ( 'NONE',  ( 0.000000000000000000, 0.000000000000000000, -0.3149606299212598381 ) ) ;
#41749=DIRECTION ( 'NONE',  ( 1.000000000000000000, 0.000000000000000000, 0.000000000000000000 ) ) ;
#41797=EDGE_CURVE ( 'NONE', #16719, #2629, #27980, .T. ) ;
#41808=CARTESIAN_POINT ( 'NONE',  ( -0.1711860128076768406, -0.1966586703792297941, -0.3122165016188725994 ) ) ;
#41852=CARTESIAN_POINT ( 'NONE',  ( -0.2559053145832481668, 0.09876138958662310230, -0.3048888299123765910 ) ) ;
#41853=CIRCLE ( 'NONE', #18922, 0.1377952755905509363 ) ;
#41869=DIRECTION ( 'NONE',  ( 1.000000000000000000, 0.000000000000000000, 0.000000000000000000 ) ) ;
#41882=CARTESIAN_POINT ( 'NONE',  ( -0.2559055118110236116, 0.1477471161312031434, -0.3149606299212598381 ) ) ;
#41919=CARTESIAN_POINT ( 'NONE',  ( 0.07097307671277083840, 0.2545179073170722450, -0.04495255068439106549 ) ) ;
#41952=DIRECTION ( 'NONE',  ( 0.000000000000000000, 0.000000000000000000, 1.000000000000000000 ) ) ;
#41954=EDGE_CURVE ( 'NONE', #42075, #16859, #20535, .T. ) ;
#41994=ORIENTED_EDGE ( 'NONE', *, *, #41954, .T. ) ;
#41997=ORIENTED_EDGE ( 'NONE', *, *, #45701, .F. ) ;
#42005=CARTESIAN_POINT ( 'NONE',  ( 0.000000000000000000, 0.000000000000000000, -0.3139606299212599483 ) ) ;
#42009=ORIENTED_EDGE ( 'NONE', *, *, #40711, .T. ) ;
#42022=DIRECTION ( 'NONE',  ( 0.000000000000000000, 0.000000000000000000, 1.000000000000000000 ) ) ;
#42075=VERTEX_POINT ( 'NONE', #46635 ) ;
#42107=CARTESIAN_POINT ( 'NONE',  ( 0.1377952755905513804, 0.000000000000000000, -0.3001770169643759867 ) ) ;
#42147=B_SPLINE_CURVE_WITH_KNOTS ( 'NONE', 3,
 ( #1179, #30462, #41416, #34286, #12482, #27107, #41656, #5257, #9813, #20814, #35452, #31165, #9344, #35224, #19877, #5735, #28043, #10041, #6190 ),
 .UNSPECIFIED., .F., .F.,
 ( 4, 2, 2, 1, 2, 2, 2, 2, 2, 4 ),
 ( 0.000000000000000000, 0.2500000000000006661, 0.3750000000000009992, 0.4375000000000009437, 0.4687500000000006661, 0.5000000000000004441, 0.6250000000000000000, 0.6875000000000000000, 0.7500000000000001110, 1.000000000000000000 ),
 .UNSPECIFIED. ) ;
#42166=DIRECTION ( 'NONE',  ( 1.000000000000000000, 0.000000000000000000, 0.000000000000000000 ) ) ;
#42178=ADVANCED_FACE ( 'NONE', ( #24846 ), #39444, .F. ) ;
#42189=CARTESIAN_POINT ( 'NONE',  ( -0.1574803149606299191, 1.928577636452524610E-17, -0.07924015748031493223 ) ) ;
#42191=VECTOR ( 'NONE', #2101, 39.37007874015748143 ) ;
#42194=DIRECTION ( 'NONE',  ( -0.000000000000000000, -0.000000000000000000, -1.000000000000000000 ) ) ;
#42210=CARTESIAN_POINT ( 'NONE',  ( -0.1062722551319878611, 0.2341365745599054971, -0.3142669362052408211 ) ) ;
#42215=DIRECTION ( 'NONE',  ( -0.000000000000000000, -0.000000000000000000, -1.000000000000000000 ) ) ;
#42239=CARTESIAN_POINT ( 'NONE',  ( 0.1279527559055118058, -0.2216206741968047289, -0.3149606299212598381 ) ) ;
#42245=FACE_OUTER_BOUND ( 'NONE', #3293, .T. ) ;
#42266=DIRECTION ( 'NONE',  ( 0.000000000000000000, 0.000000000000000000, 1.000000000000000000 ) ) ;
#42271=VECTOR ( 'NONE', #44656, 39.37007874015748143 ) ;
#42279=CONICAL_SURFACE ( 'NONE', #21626, 0.1377952755905509363, 0.9599310885968936891 ) ;
#42283=PRODUCT_DEFINITION_SHAPE ( 'NONE', 'NONE',  #24794 ) ;
#42289=CARTESIAN_POINT ( 'NONE',  ( -0.1219373188186450574, 0.2250936884182012654, -0.02739586109244948955 ) ) ;
#42342=DIRECTION ( 'NONE',  ( 1.000000000000000000, 0.000000000000000000, 0.000000000000000000 ) ) ;
#42349=ADVANCED_FACE ( 'NONE', ( #8097 ), #41672, .F. ) ;
#42350=DIRECTION ( 'NONE',  ( 0.000000000000000000, 0.000000000000000000, 1.000000000000000000 ) ) ;
#42388=CARTESIAN_POINT ( 'NONE',  ( 0.2559042684362457520, 0.05603847011398876976, -0.04023020774663194771 ) ) ;
#42405=EDGE_CURVE ( 'NONE', #954, #15682, #8807, .T. ) ;
#42408=CARTESIAN_POINT ( 'NONE',  ( 0.1985616933439197651, 0.1808545851595462772, -0.05455490385609955417 ) ) ;
#42427=CARTESIAN_POINT ( 'NONE',  ( 0.000000000000000000, 0.000000000000000000, -0.1828167807439035619 ) ) ;
#42433=AXIS2_PLACEMENT_3D ( 'NONE', #11845, #26234, #15920 ) ;
#42442=EDGE_CURVE ( 'NONE', #2951, #15186, #46275, .T. ) ;
#42444=EDGE_CURVE ( 'NONE', #24988, #8606, #43991, .T. ) ;
#42466=DIRECTION ( 'NONE',  ( -0.4230299666438205319, 0.000000000000000000, -0.9061156920180379881 ) ) ;
#42469=AXIS2_PLACEMENT_3D ( 'NONE', #10248, #24618, #14072 ) ;
#42507=CARTESIAN_POINT ( 'NONE',  ( -0.2559040288302377730, -0.08492902731590018517, -0.3070526160130827575 ) ) ;
#42531=CARTESIAN_POINT ( 'NONE',  ( 0.1377952755905511861, 0.000000000000000000, -0.05390369169704170571 ) ) ;
#42536=DIRECTION ( 'NONE',  ( -0.000000000000000000, -0.000000000000000000, -1.000000000000000000 ) ) ;
#42557=ORIENTED_EDGE ( 'NONE', *, *, #28268, .F. ) ;
#42563=ADVANCED_FACE ( 'NONE', ( #8691 ), #36989, .F. ) ;
#42564=CARTESIAN_POINT ( 'NONE',  ( 0.1377952755905510751, 0.000000000000000000, -0.3149606299212598381 ) ) ;
#42609=CARTESIAN_POINT ( 'NONE',  ( 0.2559055127798368634, 0.08170875243442862756, -0.05466978143083393860 ) ) ;
#42659=EDGE_LOOP ( 'NONE', ( #4219, #42770, #24025, #36448 ) ) ;
#42660=AXIS2_PLACEMENT_3D ( 'NONE', #4871, #37002, #40803 ) ;
#42695=CIRCLE ( 'NONE', #38895, 0.1574803149606299191 ) ;
#42725=B_SPLINE_CURVE_WITH_KNOTS ( 'NONE', 3,
 ( #17003, #21528, #38809, #31872, #13192, #45983, #39720, #27828, #31642, #2829, #13418, #24665, #42388, #21289, #39497, #28050, #17701, #28273, #14119, #42609, #46451, #10292, #6437, #28516 ),
 .UNSPECIFIED., .F., .F.,
 ( 4, 2, 2, 1, 1, 2, 2, 2, 1, 1, 1, 1, 2, 2, 4 ),
 ( 0.000000000000000000, 0.1249999999999968081, 0.1874999999999952260, 0.2187499999999943934, 0.2343749999999939493, 0.2421874999999936995, 0.2499999999999934497, 0.3749999999999907296, 0.4374999999999895084, 0.4687499999999888423, 0.4843749999999885647, 0.4921874999999884537, 0.4960937499999885092, 0.4999999999999885647, 1.000000000000000000 ),
 .UNSPECIFIED. ) ;
#42734=CARTESIAN_POINT ( 'NONE',  ( -0.05824109077986367594, 0.2618687228227554176, -0.05388431474956185269 ) ) ;
#42758=ADVANCED_FACE ( 'NONE', ( #45809 ), #14968, .F. ) ;
#42770=ORIENTED_EDGE ( 'NONE', *, *, #24035, .F. ) ;
#42797=CARTESIAN_POINT ( 'NONE',  ( -0.2559055118110235560, 0.04218462477718680492, -0.03480397727850406686 ) ) ;
#42818=DIRECTION ( 'NONE',  ( 1.000000000000000000, 0.000000000000000000, 0.000000000000000000 ) ) ;
#42939=CIRCLE ( 'NONE', #41388, 0.1574803149606299191 ) ;
#42984=EDGE_CURVE ( 'NONE', #31435, #5631, #6523, .T. ) ;
#43004=CARTESIAN_POINT ( 'NONE',  ( 0.000000000000000000, 0.000000000000000000, -0.2219368594840610276 ) ) ;
#43007=LINE ( 'NONE', #10216, #19932 ) ;
#43008=VERTEX_POINT ( 'NONE', #8873 ) ;
#43050=EDGE_CURVE ( 'NONE', #40024, #31750, #27823, .T. ) ;
#43183=EDGE_LOOP ( 'NONE', ( #12012, #10351, #957, #18642 ) ) ;
#43194=PRODUCT_DEFINITION_CONTEXT ( 'detailed design', #27872, 'design' ) ;
#43208=EDGE_CURVE ( 'NONE', #22098, #23237, #9298, .T. ) ;
#43210=EDGE_CURVE ( 'NONE', #2629, #41717, #16722, .T. ) ;
#43223=ADVANCED_FACE ( 'NONE', ( #46174 ), #11925, .F. ) ;
#43242=DIRECTION ( 'NONE',  ( 0.000000000000000000, 0.000000000000000000, 1.000000000000000000 ) ) ;
#43316=ORIENTED_EDGE ( 'NONE', *, *, #46727, .T. ) ;
#43324=EDGE_CURVE ( 'NONE', #18699, #28934, #46343, .T. ) ;
#43373=DIRECTION ( 'NONE',  ( 1.000000000000000000, 0.000000000000000000, 0.000000000000000000 ) ) ;
#43384=DIRECTION ( 'NONE',  ( 0.000000000000000000, 0.000000000000000000, 1.000000000000000000 ) ) ;
#43388=ORIENTED_EDGE ( 'NONE', *, *, #31097, .F. ) ;
#43431=CARTESIAN_POINT ( 'NONE',  ( -0.08080321177267317523, -0.2488424761940687957, -0.03960523631939861372 ) ) ;
#43438=CONICAL_SURFACE ( 'NONE', #42660, 0.2431102362204724532, 0.4367866272367255109 ) ;
#43464=DIRECTION ( 'NONE',  ( -1.000000000000000000, 0.000000000000000000, 0.000000000000000000 ) ) ;
#43470=CARTESIAN_POINT ( 'NONE',  ( -0.1574803149606299191, 0.000000000000000000, -0.04012007874015743186 ) ) ;
#43479=ORIENTED_EDGE ( 'NONE', *, *, #28615, .T. ) ;
#43507=FACE_OUTER_BOUND ( 'NONE', #3263, .T. ) ;
#43509=VERTEX_POINT ( 'NONE', #35649 ) ;
#43514=DIRECTION ( 'NONE',  ( 0.000000000000000000, 0.000000000000000000, 1.000000000000000000 ) ) ;
#43522=CARTESIAN_POINT ( 'NONE',  ( 0.08471839801908884193, -0.2465807710536996322, -0.3122165016188270803 ) ) ;
#43542=DIRECTION ( 'NONE',  ( 1.000000000000000000, 0.000000000000000000, 0.000000000000000000 ) ) ;
#43565=LINE ( 'NONE', #10536, #30279 ) ;
#43573=AXIS2_PLACEMENT_3D ( 'NONE', #30295, #26677, #41226 ) ;
#43587=CARTESIAN_POINT ( 'NONE',  ( 0.1667418150844881541, -0.1992258004382128633, -0.03573910814354441107 ) ) ;
#43591=DIRECTION ( 'NONE',  ( 1.000000000000000000, 0.000000000000000000, 0.000000000000000000 ) ) ;
#43606=ORIENTED_EDGE ( 'NONE', *, *, #33052, .T. ) ;
#43653=DIRECTION ( 'NONE',  ( 1.000000000000000000, 0.000000000000000000, 0.000000000000000000 ) ) ;
#43656=EDGE_CURVE ( 'NONE', #22098, #30017, #20362, .T. ) ;
#43713=AXIS2_PLACEMENT_3D ( 'NONE', #32554, #40163, #28479 ) ;
#43714=CARTESIAN_POINT ( 'NONE',  ( 0.000000000000000000, 0.000000000000000000, -0.2610569382242185488 ) ) ;
#43733=ORIENTED_EDGE ( 'NONE', *, *, #25714, .F. ) ;
#43766=CARTESIAN_POINT ( 'NONE',  ( 0.1225179410730680984, -0.2247584660033122572, -0.3149606299212597826 ) ) ;
#43771=CARTESIAN_POINT ( 'NONE',  ( -0.2559055118110235560, 0.08170541745154620561, -0.05466765753244264003 ) ) ;
#43778=AXIS2_PLACEMENT_3D ( 'NONE', #43004, #42536, #9740 ) ;
#43785=CIRCLE ( 'NONE', #28526, 0.2559055118110236116 ) ;
#43810=EDGE_CURVE ( 'NONE', #31906, #7313, #38561, .T. ) ;
#43821=AXIS2_PLACEMENT_3D ( 'NONE', #39791, #38867, #14426 ) ;
#43830=DIRECTION ( 'NONE',  ( 0.000000000000000000, 0.000000000000000000, 1.000000000000000000 ) ) ;
#43871=EDGE_LOOP ( 'NONE', ( #39850, #33224, #19127, #7923 ) ) ;
#43872=DIRECTION ( 'NONE',  ( 0.000000000000000000, 0.000000000000000000, 1.000000000000000000 ) ) ;
#43875=SURFACE_STYLE_FILL_AREA ( #19181 ) ;
#43888=( GEOMETRIC_REPRESENTATION_CONTEXT ( 3 ) GLOBAL_UNCERTAINTY_ASSIGNED_CONTEXT ( ( #22513 ) ) GLOBAL_UNIT_ASSIGNED_CONTEXT ( ( #7227, #30025, #40269 ) ) REPRESENTATION_CONTEXT ( 'NONE', 'WORKASPACE' ) ) ;
#43904=DIRECTION ( 'NONE',  ( 0.000000000000000000, 0.000000000000000000, 1.000000000000000000 ) ) ;
#43910=CARTESIAN_POINT ( 'NONE',  ( -0.1985616933439231790, -0.1808545851595459442, -0.05455490385610407833 ) ) ;
#43920=AXIS2_PLACEMENT_3D ( 'NONE', #23454, #4737, #38057 ) ;
#43935=EDGE_CURVE ( 'NONE', #41717, #21785, #39570, .T. ) ;
#43944=CARTESIAN_POINT ( 'NONE',  ( 2.219626494852212756E-16, 0.2954942322624074524, -0.1122047244094488277 ) ) ;
#43982=CARTESIAN_POINT ( 'NONE',  ( -0.1279527559055118058, 0.2216206741968047289, -0.3149606299212598381 ) ) ;
#43990=ORIENTED_EDGE ( 'NONE', *, *, #33900, .T. ) ;
#43991=CIRCLE ( 'NONE', #23344, 0.1377952755905511861 ) ;
#43992=CONICAL_SURFACE ( 'NONE', #20284, 0.1377952755905510196, 0.9599310885968940221 ) ;
#44018=DIRECTION ( 'NONE',  ( 1.000000000000000000, 0.000000000000000000, 0.000000000000000000 ) ) ;
#44080=EDGE_LOOP ( 'NONE', ( #46385, #34381, #12543, #4829, #41994, #16774 ) ) ;
#44087=CARTESIAN_POINT ( 'NONE',  ( -0.1063536270749164125, -0.2340938383370582132, -0.3144333452974441556 ) ) ;
#44142=CARTESIAN_POINT ( 'NONE',  ( -0.1964094517284886710, -0.1820971824355780422, -0.05295753290290854814 ) ) ;
#44175=FACE_OUTER_BOUND ( 'NONE', #2650, .T. ) ;
#44183=LINE ( 'NONE', #37726, #34536 ) ;
#44199=EDGE_LOOP ( 'NONE', ( #21642, #10827, #34632, #22515 ) ) ;
#44202=DIRECTION ( 'NONE',  ( -1.000000000000000000, 1.776356839400250070E-15, 0.000000000000000000 ) ) ;
#44208=CARTESIAN_POINT ( 'NONE',  ( -0.2559055118110236116, -0.08272504999148638793, -0.05533579728309570567 ) ) ;
#44239=LINE ( 'NONE', #11921, #35352 ) ;
#44260=DIRECTION ( 'NONE',  ( -0.000000000000000000, -0.000000000000000000, -1.000000000000000000 ) ) ;
#44261=DIRECTION ( 'NONE',  ( -0.000000000000000000, -0.000000000000000000, -1.000000000000000000 ) ) ;
#44292=CARTESIAN_POINT ( 'NONE',  ( 0.000000000000000000, 0.000000000000000000, -0.3149606299212598381 ) ) ;
#44394=EDGE_CURVE ( 'NONE', #13286, #41713, #20277, .T. ) ;
#44422=DIRECTION ( 'NONE',  ( -0.8191520442889873577, 1.003171929053519323E-16, 0.5735764363510523767 ) ) ;
#44443=ORIENTED_EDGE ( 'NONE', *, *, #10237, .F. ) ;
#44449=VECTOR ( 'NONE', #5709, 39.37007874015748143 ) ;
#44473=DIRECTION ( 'NONE',  ( 1.000000000000000000, 0.000000000000000000, 0.000000000000000000 ) ) ;
#44528=FACE_BOUND ( 'NONE', #12463, .T. ) ;
#44544=CARTESIAN_POINT ( 'NONE',  ( -0.08209939101897356650, -0.2480946695746812369, -0.3118411609178720068 ) ) ;
#44560=CARTESIAN_POINT ( 'NONE',  ( -0.2559058759996818422, 0.01250272378134492310, -0.3148280614481966388 ) ) ;
#44581=DIRECTION ( 'NONE',  ( 1.000000000000000000, 0.000000000000000000, 0.000000000000000000 ) ) ;
#44583=DIRECTION ( 'NONE',  ( -0.000000000000000000, -0.000000000000000000, -1.000000000000000000 ) ) ;
#44656=DIRECTION ( 'NONE',  ( 0.8191520442890001252, 1.003171929053535101E-16, -0.5735764363510340580 ) ) ;
#44675=ORIENTED_EDGE ( 'NONE', *, *, #26090, .F. ) ;
#44677=ORIENTED_EDGE ( 'NONE', *, *, #29963, .F. ) ;
#44695=CARTESIAN_POINT ( 'NONE',  ( -0.1792139591741687965, -0.1920237930723998898, -0.3110703821948138659 ) ) ;
#44729=CARTESIAN_POINT ( 'NONE',  ( -0.1574803149606299191, 1.928577636452524610E-17, 2.731847993664263218E-16 ) ) ;
#44768=CARTESIAN_POINT ( 'NONE',  ( 0.000000000000000000, 0.000000000000000000, -0.2748405511811023438 ) ) ;
#44800=AXIS2_PLACEMENT_3D ( 'NONE', #38285, #9771, #35414 ) ;
#44845=DIRECTION ( 'NONE',  ( -0.5000000000000007772, -0.8660254037844382635, 0.000000000000000000 ) ) ;
#44846=ORIENTED_EDGE ( 'NONE', *, *, #12788, .T. ) ;
#44918=EDGE_LOOP ( 'NONE', ( #27877, #10057, #40607, #18064 ) ) ;
#44945=CARTESIAN_POINT ( 'NONE',  ( 0.000000000000000000, 0.000000000000000000, -0.2886241641379866385 ) ) ;
#44987=DIRECTION ( 'NONE',  ( 1.000000000000000000, 0.000000000000000000, 0.000000000000000000 ) ) ;
#45015=EDGE_LOOP ( 'NONE', ( #35614, #20480, #7132, #43316 ) ) ;
#45017=CARTESIAN_POINT ( 'NONE',  ( -0.01090721357322046656, -0.2891969495697969683, -0.2957398093695223773 ) ) ;
#45048=CARTESIAN_POINT ( 'NONE',  ( 0.04877781748284810287, 0.2673323462082016211, -0.06129781628411318933 ) ) ;
#45092=CARTESIAN_POINT ( 'NONE',  ( 4.268512490100409430E-16, 0.2954942322624074524, -0.2921040715117803055 ) ) ;
#45093=CARTESIAN_POINT ( 'NONE',  ( -0.1377952755905510751, 0.000000000000000000, -0.02633646578327370619 ) ) ;
#45118=DIRECTION ( 'NONE',  ( 0.000000000000000000, 0.000000000000000000, 1.000000000000000000 ) ) ;
#45129=ORIENTED_EDGE ( 'NONE', *, *, #43656, .F. ) ;
#45143=CARTESIAN_POINT ( 'NONE',  ( 0.000000000000000000, 0.000000000000000000, -0.02633646578327370619 ) ) ;
#45156=EDGE_LOOP ( 'NONE', ( #12417, #24654, #35807, #14687 ) ) ;
#45173=CARTESIAN_POINT ( 'NONE',  ( -0.1913749512857115809, -0.1850038654769096402, -0.3090319486758666412 ) ) ;
#45240=AXIS2_PLACEMENT_3D ( 'NONE', #31348, #9533, #38761 ) ;
#45257=ORIENTED_EDGE ( 'NONE', *, *, #11110, .F. ) ;
#45312=EDGE_CURVE ( 'NONE', #5631, #31435, #6980, .T. ) ;
#45359=LINE ( 'NONE', #27907, #28171 ) ;
#45367=DIRECTION ( 'NONE',  ( 1.000000000000000000, 0.000000000000000000, 0.000000000000000000 ) ) ;
#45446=AXIS2_PLACEMENT_3D ( 'NONE', #39928, #14320, #25344 ) ;
#45447=CARTESIAN_POINT ( 'NONE',  ( 0.2559055118110236116, 0.1477471161312027548, -0.3149606299212598381 ) ) ;
#45480=DIRECTION ( 'NONE',  ( 0.000000000000000000, 0.000000000000000000, 1.000000000000000000 ) ) ;
#45512=ORIENTED_EDGE ( 'NONE', *, *, #32883, .F. ) ;
#45523=CARTESIAN_POINT ( 'NONE',  ( 0.08916369672653763623, 0.2440155479553977047, -0.03573910814354051141 ) ) ;
#45544=EDGE_CURVE ( 'NONE', #15682, #21809, #11667, .T. ) ;
#45552=CARTESIAN_POINT ( 'NONE',  ( -0.2559055118110236116, -0.04346162977120471976, -0.03525533988057330537 ) ) ;
#45592=DIRECTION ( 'NONE',  ( -0.000000000000000000, -0.000000000000000000, -1.000000000000000000 ) ) ;
#45610=CARTESIAN_POINT ( 'NONE',  ( 0.1377952755905509363, 1.687505431895956106E-17, -0.1436967020037460685 ) ) ;
#45614=ORIENTED_EDGE ( 'NONE', *, *, #10415, .T. ) ;
#45634=EDGE_CURVE ( 'NONE', #28525, #9873, #19058, .T. ) ;
#45660=CONICAL_SURFACE ( 'NONE', #36530, 0.1574803149606299191, 0.9599310885968735940 ) ;
#45673=CARTESIAN_POINT ( 'NONE',  ( 0.000000000000000000, 0.000000000000000000, -0.2357204724409448504 ) ) ;
#45687=CARTESIAN_POINT ( 'NONE',  ( -0.2559057194709206673, 0.06872035568902440383, -0.3097284958882876582 ) ) ;
#45701=EDGE_CURVE ( 'NONE', #3606, #873, #38348, .T. ) ;
#45707=DIRECTION ( 'NONE',  ( 0.000000000000000000, 0.000000000000000000, 1.000000000000000000 ) ) ;
#45803=ORIENTED_EDGE ( 'NONE', *, *, #1941, .F. ) ;
#45805=CARTESIAN_POINT ( 'NONE',  ( -0.1279527559055118058, 0.2216206741968047289, -0.3149606299212598381 ) ) ;
#45809=FACE_OUTER_BOUND ( 'NONE', #44918, .T. ) ;
#45831=DIRECTION ( 'NONE',  ( 0.000000000000000000, 0.000000000000000000, 1.000000000000000000 ) ) ;
#45855=VERTEX_POINT ( 'NONE', #17123 ) ;
#45861=CIRCLE ( 'NONE', #32900, 0.1377952755905511861 ) ;
#45872=CARTESIAN_POINT ( 'NONE',  ( -0.2559051007267882372, -0.06201594832447591965, -0.3107242013313469275 ) ) ;
#45878=ORIENTED_EDGE ( 'NONE', *, *, #8159, .T. ) ;
#45928=CARTESIAN_POINT ( 'NONE',  ( 0.000000000000000000, 0.000000000000000000, -0.3149606299212598381 ) ) ;
#45937=DIRECTION ( 'NONE',  ( 0.000000000000000000, 0.000000000000000000, 1.000000000000000000 ) ) ;
#45942=CARTESIAN_POINT ( 'NONE',  ( 0.1574803149606299191, 1.928577636452524918E-17, -0.1966003937007873570 ) ) ;
#45963=CARTESIAN_POINT ( 'NONE',  ( 0.1567662409572586624, 0.000000000000000000, -0.0004999999999998990712 ) ) ;
#45964=AXIS2_PLACEMENT_3D ( 'NONE', #3589, #8773, #1098 ) ;
#45965=ORIENTED_EDGE ( 'NONE', *, *, #46150, .F. ) ;
#45983=CARTESIAN_POINT ( 'NONE',  ( 0.2559044495549840925, 0.03407473760173215793, -0.03222949210965551231 ) ) ;
#45992=ORIENTED_EDGE ( 'NONE', *, *, #18307, .F. ) ;
#46008=CARTESIAN_POINT ( 'NONE',  ( 0.1432458882846917303, 0.2127911801009324810, -0.02834147079956138293 ) ) ;
#46023=DIRECTION ( 'NONE',  ( 0.000000000000000000, 0.000000000000000000, 1.000000000000000000 ) ) ;
#46054=CARTESIAN_POINT ( 'NONE',  ( 0.2559055118110236671, -0.07588913166135959065, -0.3086013035114750225 ) ) ;
#46067=LINE ( 'NONE', #24054, #29163 ) ;
#46089=CARTESIAN_POINT ( 'NONE',  ( -0.04075098337902038209, -0.2719666410387886479, -0.06815351164855749933 ) ) ;
#46112=CARTESIAN_POINT ( 'NONE',  ( -0.2559055234657572897, -0.07599696328693686387, -0.3085855680301413106 ) ) ;
#46150=EDGE_CURVE ( 'NONE', #28768, #3799, #37454, .T. ) ;
#46154=ORIENTED_EDGE ( 'NONE', *, *, #7746, .T. ) ;
#46158=ORIENTED_EDGE ( 'NONE', *, *, #43810, .F. ) ;
#46174=FACE_OUTER_BOUND ( 'NONE', #34299, .T. ) ;
#46205=ORIENTED_EDGE ( 'NONE', *, *, #33032, .T. ) ;
#46208=ORIENTED_EDGE ( 'NONE', *, *, #18307, .T. ) ;
#46233=VECTOR ( 'NONE', #80, 39.37007874015748143 ) ;
#46234=EDGE_CURVE ( 'NONE', #9930, #28164, #5090, .T. ) ;
#46236=CARTESIAN_POINT ( 'NONE',  ( 0.1751023000384251405, -0.1943988721995016100, -0.03960523631944738027 ) ) ;
#46244=EDGE_LOOP ( 'NONE', ( #4303, #2692, #26163, #35557, #35045 ) ) ;
#46275=CIRCLE ( 'NONE', #10349, 0.1574803149606299191 ) ;
#46293=CARTESIAN_POINT ( 'NONE',  ( 0.2559055118110236671, -0.08465028870289853513, -0.3071002465948138305 ) ) ;
#46343=CIRCLE ( 'NONE', #29580, 0.1574803149606299191 ) ;
#46385=ORIENTED_EDGE ( 'NONE', *, *, #6602, .F. ) ;
#46387=LINE ( 'NONE', #20046, #14654 ) ;
#46398=CARTESIAN_POINT ( 'NONE',  ( -0.1377952755905511861, 1.808041534174241898E-17, -0.1712639279175142137 ) ) ;
#46451=CARTESIAN_POINT ( 'NONE',  ( 0.2559055128465877460, 0.08195185539867717861, -0.05482843030950571711 ) ) ;
#46456=CIRCLE ( 'NONE', #38814, 0.1377952755905513804 ) ;
#46475=CARTESIAN_POINT ( 'NONE',  ( 0.09162190804155555257, -0.2425962989909497547, -0.03472289316814022170 ) ) ;
#46486=CIRCLE ( 'NONE', #33500, 0.1377952755905510474 ) ;
#46516=EDGE_CURVE ( 'NONE', #38506, #14850, #26949, .T. ) ;
#46520=CONICAL_SURFACE ( 'NONE', #2135, 0.1377952755905509641, 0.9599310885968941331 ) ;
#46528=CARTESIAN_POINT ( 'NONE',  ( 0.2559055118110236116, -0.07522986544523073416, -0.3087092415967106485 ) ) ;
#46542=CARTESIAN_POINT ( 'NONE',  ( 0.1657973489140633916, -0.1997733981812202797, -0.3128311589625492606 ) ) ;
#46581=CARTESIAN_POINT ( 'NONE',  ( 0.1377952755905509363, 1.687505431895956106E-17, -0.1045766232635885612 ) ) ;
#46586=EDGE_LOOP ( 'NONE', ( #44443, #12844, #2027, #33750 ) ) ;
#46587=AXIS2_PLACEMENT_3D ( 'NONE', #39199, #9990, #21232 ) ;
#46589=CARTESIAN_POINT ( 'NONE',  ( -0.1751023000383840345, 0.1943988721995235924, -0.03960523631940795347 ) ) ;
#46604=CARTESIAN_POINT ( 'NONE',  ( 0.1574803149606299191, 0.000000000000000000, -0.2748405511811023438 ) ) ;
#46635=CARTESIAN_POINT ( 'NONE',  ( 0.2559055118110236116, 0.1477471161312045311, -0.2921040715117803055 ) ) ;
#46644=EDGE_LOOP ( 'NONE', ( #11525, #41136, #17825, #29195 ) ) ;
#46652=CARTESIAN_POINT ( 'NONE',  ( -0.2559055118110236116, 0.1477471161312031434, -0.1122047244094468571 ) ) ;
#46680=AXIS2_PLACEMENT_3D ( 'NONE', #13617, #28258, #42818 ) ;
#46713=AXIS2_PLACEMENT_3D ( 'NONE', #23474, #38076, #18902 ) ;
#46719=VECTOR ( 'NONE', #20473, 39.37007874015748143 ) ;
#46727=EDGE_CURVE ( 'NONE', #20308, #39783, #30791, .T. ) ;
#46789=EDGE_CURVE ( 'NONE', #4309, #21602, #43785, .T. ) ;
#46793=CIRCLE ( 'NONE', #83, 0.2559055118110236116 ) ;
#46825=CARTESIAN_POINT ( 'NONE',  ( -0.08530144295877870042, 0.2462454212078929172, -0.03730110279446391397 ) ) ;
#46909=DIRECTION ( 'NONE',  ( 0.000000000000000000, 0.000000000000000000, 1.000000000000000000 ) ) ;
#46950=CARTESIAN_POINT ( 'NONE',  ( 0.000000000000000000, 0.000000000000000000, -0.1045766232635885612 ) ) ;
#46988=CIRCLE ( 'NONE', #7177, 0.1377952755905511861 ) ;
#47044=ORIENTED_EDGE ( 'NONE', *, *, #43935, .T. ) ;
#47142=CARTESIAN_POINT ( 'NONE',  ( -0.2559055118110236116, 0.07057771752877874116, -0.04780316061551689866 ) ) ;
#47154=CYLINDRICAL_SURFACE ( 'NONE', #32232, 0.1377952755905510751 ) ;
#47201=CARTESIAN_POINT ( 'NONE',  ( 0.05949606008254617467, -0.2611441659580287511, -0.05295753290290579340 ) ) ;
#47203=CARTESIAN_POINT ( 'NONE',  ( 0.000000000000000000, 0.000000000000000000, -0.1436967020037460685 ) ) ;
#47313=AXIS2_PLACEMENT_3D ( 'NONE', #3286, #28017, #10015 ) ;
#47376=CYLINDRICAL_SURFACE ( 'NONE', #45446, 0.1574803149606299191 ) ;
#47382=CARTESIAN_POINT ( 'NONE',  ( -0.2559055118110236116, 0.05914120415906069794, -0.04157189868441935748 ) ) ;
#47393=FACE_OUTER_BOUND ( 'NONE', #28931, .T. ) ;
#47424=ORIENTED_EDGE ( 'NONE', *, *, #26869, .T. ) ;
#47438=ORIENTED_EDGE ( 'NONE', *, *, #17864, .F. ) ;
ENDSEC;
END-ISO-10303-21;
